ISO-10303-21;
HEADER;
FILE_DESCRIPTION (('STEP AP203'),
    '1' );
FILE_NAME ('MAS-409-Body.step',
    '2026-10-07T20:09:13',
    ( '' ),
    ( '' ),
    'SwSTEP 2.0',
    'SolidWorks 2024',
    '' );
FILE_SCHEMA (( 'AUTOMOTIVE_DESIGN' ));
ENDSEC;

DATA;
#7=CARTESIAN_POINT ( 'NONE',  ( 0.8119709581221709049, 2.978485840173427324, -1.588368860739399313 ) ) ;
#12=CARTESIAN_POINT ( 'NONE',  ( 0.4200000000000001510, 0.05000000000000028727, -2.565999999999999837 ) ) ;
#21=VECTOR ( 'NONE', #10740, 39.37007874015748143 ) ;
#37=VECTOR ( 'NONE', #16324, 39.37007874015748143 ) ;
#52=ORIENTED_EDGE ( 'NONE', *, *, #22032, .T. ) ;
#59=EDGE_CURVE ( 'NONE', #5903, #21880, #9041, .T. ) ;
#69=CARTESIAN_POINT ( 'NONE',  ( 2.055580586463031434, 2.740000000000000213, -2.936000000000001720 ) ) ;
#77=EDGE_LOOP ( 'NONE', ( #1888, #18822, #18555, #19530 ) ) ;
#84=CARTESIAN_POINT ( 'NONE',  ( 0.3950000000000000178, 2.740039370078740433, -1.966000000000000192 ) ) ;
#89=EDGE_CURVE ( 'NONE', #12827, #10130, #5133, .T. ) ;
#91=LINE ( 'NONE', #7534, #15165 ) ;
#95=DIRECTION ( 'NONE',  ( -0.4995222938423184988, -0.04370253788966844966, 0.8651979924482664508 ) ) ;
#97=EDGE_CURVE ( 'NONE', #19422, #8315, #12597, .T. ) ;
#105=ORIENTED_EDGE ( 'NONE', *, *, #5573, .F. ) ;
#122=ORIENTED_EDGE ( 'NONE', *, *, #2601, .F. ) ;
#127=DIRECTION ( 'NONE',  ( -0.6125180959723208751, -0.6125180959723208751, 0.4996430367901520953 ) ) ;
#133=PLANE ( 'NONE',  #11743 ) ;
#143=DIRECTION ( 'NONE',  ( 0.7071067811865475727, -0.7071067811865475727, 0.000000000000000000 ) ) ;
#145=CARTESIAN_POINT ( 'NONE',  ( 0.9995881047227681560, 2.471730513698206178, -1.219071084208098732 ) ) ;
#169=CARTESIAN_POINT ( 'NONE',  ( 0.4449999999999992850, 0.000000000000000000, -0.4288675134594802096 ) ) ;
#190=VECTOR ( 'NONE', #20560, 39.37007874015748143 ) ;
#199=EDGE_CURVE ( 'NONE', #21090, #21943, #17206, .T. ) ;
#207=FACE_OUTER_BOUND ( 'NONE', #7341, .T. ) ;
#213=DIRECTION ( 'NONE',  ( 0.000000000000000000, 0.000000000000000000, -1.000000000000000000 ) ) ;
#229=PLANE ( 'NONE',  #11115 ) ;
#235=CARTESIAN_POINT ( 'NONE',  ( 0.4450000000000002842, 0.05000000000000028727, -2.591000000000000192 ) ) ;
#261=DIRECTION ( 'NONE',  ( -0.5773502691896257311, -0.5773502691896257311, 0.5773502691896257311 ) ) ;
#265=ADVANCED_FACE ( 'NONE', ( #22443 ), #4898, .F. ) ;
#279=PLANE ( 'NONE',  #11488 ) ;
#285=ORIENTED_EDGE ( 'NONE', *, *, #22981, .F. ) ;
#288=ORIENTED_EDGE ( 'NONE', *, *, #4311, .T. ) ;
#293=LINE ( 'NONE', #9080, #3063 ) ;
#298=PLANE ( 'NONE',  #11943 ) ;
#311=ORIENTED_EDGE ( 'NONE', *, *, #12442, .F. ) ;
#332=CARTESIAN_POINT ( 'NONE',  ( 2.284599161994749217, 2.687712728237018567, -2.476240473580834323 ) ) ;
#337=ORIENTED_EDGE ( 'NONE', *, *, #3360, .F. ) ;
#341=AXIS2_PLACEMENT_3D ( 'NONE', #20184, #3472, #18351 ) ;
#348=EDGE_LOOP ( 'NONE', ( #13704, #13616, #8362, #11968, #22860, #19781, #8020, #11715 ) ) ;
#363=VERTEX_POINT ( 'NONE', #13911 ) ;
#389=ORIENTED_EDGE ( 'NONE', *, *, #20656, .T. ) ;
#396=AXIS2_PLACEMENT_3D ( 'NONE', #11256, #143, #18802 ) ;
#397=VERTEX_POINT ( 'NONE', #8282 ) ;
#398=DIRECTION ( 'NONE',  ( -1.000000000000000000, 0.000000000000000000, 0.000000000000000000 ) ) ;
#401=CARTESIAN_POINT ( 'NONE',  ( 0.05000000000000028727, 2.740000000000000213, -0.9255073213098983231 ) ) ;
#420=DIRECTION ( 'NONE',  ( -0.8651979924482658957, 0.04370253788966848435, 0.4995222938423194425 ) ) ;
#435=ORIENTED_EDGE ( 'NONE', *, *, #5401, .F. ) ;
#476=CARTESIAN_POINT ( 'NONE',  ( 0.4901945818292207657, 2.760194581829221061, -0.07019458182922092004 ) ) ;
#504=CARTESIAN_POINT ( 'NONE',  ( 2.911000000000000032, 0.04999999999999919092, 0.000000000000000000 ) ) ;
#509=ADVANCED_FACE ( 'NONE', ( #18279 ), #1216, .F. ) ;
#512=CARTESIAN_POINT ( 'NONE',  ( 2.114711001306381011, 2.690000000000002167, -2.986000000000000210 ) ) ;
#527=ORIENTED_EDGE ( 'NONE', *, *, #15962, .T. ) ;
#537=VECTOR ( 'NONE', #2199, 39.37007874015748143 ) ;
#540=CARTESIAN_POINT ( 'NONE',  ( 0.8352479138593175145, 0.000000000000000000, -3.011000000000000565 ) ) ;
#544=VERTEX_POINT ( 'NONE', #20232 ) ;
#548=ORIENTED_EDGE ( 'NONE', *, *, #15332, .T. ) ;
#558=( GEOMETRIC_REPRESENTATION_CONTEXT ( 3 ) GLOBAL_UNCERTAINTY_ASSIGNED_CONTEXT ( ( #11693 ) ) GLOBAL_UNIT_ASSIGNED_CONTEXT ( ( #9433, #22474, #11881 ) ) REPRESENTATION_CONTEXT ( 'NONE', 'WORKASPACE' ) );
#566=EDGE_CURVE ( 'NONE', #9581, #14200, #18166, .T. ) ;
#570=CARTESIAN_POINT ( 'NONE',  ( 0.3699999999999995515, 0.000000000000000000, -1.922698729810778273 ) ) ;
#571=CARTESIAN_POINT ( 'NONE',  ( 1.682181019992768034, 2.405292355953585481, -2.038697013607245978 ) ) ;
#636=PLANE ( 'NONE',  #7128 ) ;
#638=ORIENTED_EDGE ( 'NONE', *, *, #2660, .F. ) ;
#639=DIRECTION ( 'NONE',  ( 0.6399207742898923579, 0.6399207742898924689, -0.4254442446013919077 ) ) ;
#657=EDGE_LOOP ( 'NONE', ( #12785, #23808, #23001, #6028, #16754 ) ) ;
#671=ORIENTED_EDGE ( 'NONE', *, *, #3179, .F. ) ;
#674=VECTOR ( 'NONE', #17420, 39.37007874015748143 ) ;
#690=CARTESIAN_POINT ( 'NONE',  ( 0.9244709581221690620, 2.291712385858714285, -1.333428253224823168 ) ) ;
#695=DIRECTION ( 'NONE',  ( -0.4999999999999760192, 0.000000000000000000, 0.8660254037844524744 ) ) ;
#713=DIRECTION ( 'NONE',  ( 1.707404996040164512E-16, 0.000000000000000000, -1.000000000000000000 ) ) ;
#727=ORIENTED_EDGE ( 'NONE', *, *, #16674, .T. ) ;
#728=AXIS2_PLACEMENT_3D ( 'NONE', #16579, #7312, #21932 ) ;
#729=DIRECTION ( 'NONE',  ( 0.8660254037844383745, -3.466132199608281475E-18, 0.5000000000000004441 ) ) ;
#732=FACE_OUTER_BOUND ( 'NONE', #19787, .T. ) ;
#740=CARTESIAN_POINT ( 'NONE',  ( 0.000000000000000000, 2.689999999999999947, -0.8847213396323272416 ) ) ;
#748=PLANE ( 'NONE',  #12096 ) ;
#760=VECTOR ( 'NONE', #8554, 39.37007874015748854 ) ;
#776=EDGE_CURVE ( 'NONE', #12827, #14874, #23357, .T. ) ;
#792=VECTOR ( 'NONE', #15978, 39.37007874015748854 ) ;
#810=VECTOR ( 'NONE', #17058, 39.37007874015748143 ) ;
#815=VECTOR ( 'NONE', #18919, 39.37007874015748143 ) ;
#821=ORIENTED_EDGE ( 'NONE', *, *, #7465, .T. ) ;
#826=AXIS2_PLACEMENT_3D ( 'NONE', #7138, #23693, #20181 ) ;
#830=EDGE_CURVE ( 'NONE', #2961, #10685, #3831, .T. ) ;
#836=ORIENTED_EDGE ( 'NONE', *, *, #1140, .F. ) ;
#837=CARTESIAN_POINT ( 'NONE',  ( 0.3950000000000000733, 0.000000000000000000, -0.4000000000000000222 ) ) ;
#847=EDGE_LOOP ( 'NONE', ( #20067, #11056, #922, #8581 ) ) ;
#856=FACE_OUTER_BOUND ( 'NONE', #8804, .T. ) ;
#872=AXIS2_PLACEMENT_3D ( 'NONE', #24104, #22401, #18505 ) ;
#878=DIRECTION ( 'NONE',  ( -0.7071067811865477948, -0.7071067811865473507, -1.207317650931791104E-16 ) ) ;
#880=DIRECTION ( 'NONE',  ( 0.8635502596144278842, 0.07555085810113110201, 0.4985709748471496838 ) ) ;
#886=PLANE ( 'NONE',  #18636 ) ;
#906=EDGE_CURVE ( 'NONE', #14487, #19422, #17768, .T. ) ;
#910=ADVANCED_FACE ( 'NONE', ( #20320 ), #9225, .F. ) ;
#912=ORIENTED_EDGE ( 'NONE', *, *, #19552, .F. ) ;
#913=DIRECTION ( 'NONE',  ( 0.9618236294503443862, 0.08414866388826429400, -0.2604118050257833716 ) ) ;
#922=ORIENTED_EDGE ( 'NONE', *, *, #3016, .F. ) ;
#923=FACE_OUTER_BOUND ( 'NONE', #13557, .T. ) ;
#931=LINE ( 'NONE', #3013, #4292 ) ;
#968=VECTOR ( 'NONE', #17566, 39.37007874015748143 ) ;
#972=CARTESIAN_POINT ( 'NONE',  ( 2.986000000000000210, 2.664999999999999591, -2.591000000000000636 ) ) ;
#984=DIRECTION ( 'NONE',  ( 0.000000000000000000, 0.000000000000000000, -1.000000000000000000 ) ) ;
#986=CARTESIAN_POINT ( 'NONE',  ( 2.911000000000000032, 0.04999999999999919092, 0.000000000000000000 ) ) ;
#1009=DIRECTION ( 'NONE',  ( 0.8660254037844434816, 0.000000000000000000, -0.4999999999999913403 ) ) ;
#1019=DIRECTION ( 'NONE',  ( 0.5598087876773550908, -0.5598087876773550908, 0.6109240889655765949 ) ) ;
#1032=VERTEX_POINT ( 'NONE', #13470 ) ;
#1042=DIRECTION ( 'NONE',  ( 0.000000000000000000, 0.000000000000000000, -1.000000000000000000 ) ) ;
#1052=DIRECTION ( 'NONE',  ( 0.000000000000000000, -1.000000000000000000, 0.000000000000000000 ) ) ;
#1054=PLANE ( 'NONE',  #22884 ) ;
#1066=VERTEX_POINT ( 'NONE', #16001 ) ;
#1076=DIRECTION ( 'NONE',  ( 0.000000000000000000, 0.000000000000000000, -1.000000000000000000 ) ) ;
#1094=CARTESIAN_POINT ( 'NONE',  ( 0.6366666666666670471, 2.473333333333333162, -2.782666666666667066 ) ) ;
#1103=LINE ( 'NONE', #2696, #792 ) ;
#1107=DIRECTION ( 'NONE',  ( 0.000000000000000000, 0.000000000000000000, -1.000000000000000000 ) ) ;
#1118=DIRECTION ( 'NONE',  ( -0.4999999999999911737, 0.000000000000000000, 0.8660254037844437036 ) ) ;
#1131=EDGE_CURVE ( 'NONE', #11997, #14781, #18722, .T. ) ;
#1140=EDGE_CURVE ( 'NONE', #18221, #8054, #19506, .T. ) ;
#1143=CARTESIAN_POINT ( 'NONE',  ( 2.311159733195646826, 2.661358883302036293, -2.462236895612579968 ) ) ;
#1154=VERTEX_POINT ( 'NONE', #6579 ) ;
#1160=ORIENTED_EDGE ( 'NONE', *, *, #11151, .T. ) ;
#1163=DIRECTION ( 'NONE',  ( 0.000000000000000000, 0.000000000000000000, -1.000000000000000000 ) ) ;
#1174=DIRECTION ( 'NONE',  ( 0.000000000000000000, 0.000000000000000000, -1.000000000000000000 ) ) ;
#1177=EDGE_CURVE ( 'NONE', #9859, #1821, #19623, .T. ) ;
#1181=VECTOR ( 'NONE', #1052, 39.37007874015748143 ) ;
#1183=DIRECTION ( 'NONE',  ( 1.000000000000000000, 0.000000000000000000, -6.148297094540788948E-16 ) ) ;
#1184=VERTEX_POINT ( 'NONE', #11850 ) ;
#1195=CARTESIAN_POINT ( 'NONE',  ( 1.573500000000000343, 0.5250000000000000222, -0.3524999999999999800 ) ) ;
#1198=ORIENTED_EDGE ( 'NONE', *, *, #8725, .F. ) ;
#1216=CYLINDRICAL_SURFACE ( 'NONE', #8821, 0.1874999999999998335 ) ;
#1251=ORIENTED_EDGE ( 'NONE', *, *, #10383, .T. ) ;
#1253=EDGE_LOOP ( 'NONE', ( #10356, #5784, #15552, #17852 ) ) ;
#1276=ORIENTED_EDGE ( 'NONE', *, *, #23443, .F. ) ;
#1282=CARTESIAN_POINT ( 'NONE',  ( 0.3247595264191661668, 2.291712385858714729, -0.9871846966950065250 ) ) ;
#1288=EDGE_CURVE ( 'NONE', #18221, #10945, #12489, .T. ) ;
#1304=ORIENTED_EDGE ( 'NONE', *, *, #22713, .F. ) ;
#1326=FACE_OUTER_BOUND ( 'NONE', #19357, .T. ) ;
#1348=ORIENTED_EDGE ( 'NONE', *, *, #12774, .T. ) ;
#1349=CARTESIAN_POINT ( 'NONE',  ( 2.986000000000000210, 0.05000000000000028727, -2.541000000000000369 ) ) ;
#1350=LINE ( 'NONE', #18054, #23745 ) ;
#1371=FACE_OUTER_BOUND ( 'NONE', #3579, .T. ) ;
#1381=CARTESIAN_POINT ( 'NONE',  ( 0.8977114317029943891, 2.978485840173427324, -0.6898620042323803103 ) ) ;
#1383=DIRECTION ( 'NONE',  ( 0.000000000000000000, 0.000000000000000000, -1.000000000000000000 ) ) ;
#1397=AXIS2_PLACEMENT_3D ( 'NONE', #12766, #12889, #16528 ) ;
#1410=ORIENTED_EDGE ( 'NONE', *, *, #9910, .T. ) ;
#1416=ORIENTED_EDGE ( 'NONE', *, *, #7936, .F. ) ;
#1420=CARTESIAN_POINT ( 'NONE',  ( 1.573500000000000343, 2.683750000000000746, -1.818749999999999645 ) ) ;
#1421=DIRECTION ( 'NONE',  ( -1.493785812010397745E-17, 1.000000000000000000, 0.000000000000000000 ) ) ;
#1440=DIRECTION ( 'NONE',  ( 0.08715574274765829077, -0.9961946980917454342, 0.000000000000000000 ) ) ;
#1471=CARTESIAN_POINT ( 'NONE',  ( 1.573500000000000343, -3.414809992080329023E-17, -0.3524999999999999800 ) ) ;
#1477=DIRECTION ( 'NONE',  ( 0.6123724356957941373, -0.7071067811865463515, -0.3535533905932771725 ) ) ;
#1485=CARTESIAN_POINT ( 'NONE',  ( 2.936000000000001720, 2.740000000000000213, 0.000000000000000000 ) ) ;
#1489=DIRECTION ( 'NONE',  ( 0.2813865959466322897, 0.6785357704725523131, 0.6785357704725568651 ) ) ;
#1490=PLANE ( 'NONE',  #13978 ) ;
#1491=EDGE_LOOP ( 'NONE', ( #15068, #11395, #22662, #9331 ) ) ;
#1502=DIRECTION ( 'NONE',  ( 0.8154147512597614833, -0.5737842049460694094, -0.07661898969830084616 ) ) ;
#1504=DIRECTION ( 'NONE',  ( 0.000000000000000000, -1.000000000000000000, 1.493785812010397437E-17 ) ) ;
#1523=DIRECTION ( 'NONE',  ( -0.7071067811865435759, -0.7071067811865514585, -9.185433182841584085E-17 ) ) ;
#1546=VECTOR ( 'NONE', #639, 39.37007874015748854 ) ;
#1549=ORIENTED_EDGE ( 'NONE', *, *, #9432, .T. ) ;
#1550=EDGE_CURVE ( 'NONE', #544, #14874, #20510, .T. ) ;
#1557=EDGE_CURVE ( 'NONE', #3473, #21943, #10774, .T. ) ;
#1558=ORIENTED_EDGE ( 'NONE', *, *, #22382, .T. ) ;
#1560=CARTESIAN_POINT ( 'NONE',  ( 2.350334729443114501, -0.003191536374479159947, -2.986000000000000210 ) ) ;
#1592=ORIENTED_EDGE ( 'NONE', *, *, #14489, .T. ) ;
#1598=ORIENTED_EDGE ( 'NONE', *, *, #18132, .F. ) ;
#1607=DIRECTION ( 'NONE',  ( 0.000000000000000000, 0.000000000000000000, -1.000000000000000000 ) ) ;
#1648=ORIENTED_EDGE ( 'NONE', *, *, #10070, .T. ) ;
#1657=VECTOR ( 'NONE', #16201, 39.37007874015748854 ) ;
#1661=VERTEX_POINT ( 'NONE', #21854 ) ;
#1674=LINE ( 'NONE', #20214, #21390 ) ;
#1689=ADVANCED_FACE ( 'NONE', ( #23788 ), #18318, .T. ) ;
#1704=VECTOR ( 'NONE', #8060, 39.37007874015748143 ) ;
#1721=EDGE_CURVE ( 'NONE', #23820, #20507, #6226, .T. ) ;
#1736=EDGE_CURVE ( 'NONE', #1821, #24062, #11611, .T. ) ;
#1738=CARTESIAN_POINT ( 'NONE',  ( 1.069687032369026403, 2.453197021783230625, -1.096034709530573359 ) ) ;
#1742=AXIS2_PLACEMENT_3D ( 'NONE', #5975, #23036, #13317 ) ;
#1756=AXIS2_PLACEMENT_3D ( 'NONE', #13765, #2772, #12189 ) ;
#1762=FACE_OUTER_BOUND ( 'NONE', #21500, .T. ) ;
#1764=EDGE_LOOP ( 'NONE', ( #12031, #20826, #727, #18229, #8979, #5602, #22234, #9828, #12167, #16375 ) ) ;
#1776=VECTOR ( 'NONE', #21022, 39.37007874015748854 ) ;
#1779=DIRECTION ( 'NONE',  ( 0.8651979924482661177, -0.04370253788966847047, -0.4995222938423191650 ) ) ;
#1793=ORIENTED_EDGE ( 'NONE', *, *, #14324, .F. ) ;
#1797=DIRECTION ( 'NONE',  ( -0.4999999999999877320, 0.000000000000000000, 0.8660254037844458130 ) ) ;
#1821=VERTEX_POINT ( 'NONE', #9533 ) ;
#1830=PLANE ( 'NONE',  #2830 ) ;
#1835=AXIS2_PLACEMENT_3D ( 'NONE', #20819, #4347, #2046 ) ;
#1847=DIRECTION ( 'NONE',  ( 0.7071067811865474617, -0.000000000000000000, -0.7071067811865474617 ) ) ;
#1851=LINE ( 'NONE', #16735, #1704 ) ;
#1876=CARTESIAN_POINT ( 'NONE',  ( 1.658214884748263618, 0.000000000000000000, -2.174029041877829638 ) ) ;
#1878=FACE_OUTER_BOUND ( 'NONE', #4340, .T. ) ;
#1886=ORIENTED_EDGE ( 'NONE', *, *, #11812, .T. ) ;
#1888=ORIENTED_EDGE ( 'NONE', *, *, #16334, .F. ) ;
#1897=AXIS2_PLACEMENT_3D ( 'NONE', #4811, #12278, #19694 ) ;
#1908=LINE ( 'NONE', #20208, #17736 ) ;
#1909=LINE ( 'NONE', #16670, #18816 ) ;
#1910=ORIENTED_EDGE ( 'NONE', *, *, #22477, .F. ) ;
#1921=LINE ( 'NONE', #10960, #17040 ) ;
#1923=DIRECTION ( 'NONE',  ( 0.7071067811865474617, 1.239037099348071290E-16, 0.7071067811865474617 ) ) ;
#1943=VERTEX_POINT ( 'NONE', #8056 ) ;
#1952=PLANE ( 'NONE',  #19774 ) ;
#1954=VERTEX_POINT ( 'NONE', #15504 ) ;
#1960=CIRCLE ( 'NONE', #11316, 0.4625000000000000777 ) ;
#1970=CARTESIAN_POINT ( 'NONE',  ( 2.170194434256479177, 2.290013683160381674, -2.965986316839620773 ) ) ;
#1971=DIRECTION ( 'NONE',  ( -0.4985709748471498504, -0.07555085810113110201, -0.8635502596144276621 ) ) ;
#1985=AXIS2_PLACEMENT_3D ( 'NONE', #8316, #6979, #21848 ) ;
#1990=CARTESIAN_POINT ( 'NONE',  ( 0.3214243565000137748, 2.693118229757915039, -1.028079841261090754 ) ) ;
#1995=LENGTH_MEASURE_WITH_UNIT ( LENGTH_MEASURE( 0.02539999999999999897 ), #19058 );
#2035=DIRECTION ( 'NONE',  ( -0.000000000000000000, -1.000000000000000000, -0.000000000000000000 ) ) ;
#2046=DIRECTION ( 'NONE',  ( 0.8660254037844382635, 0.000000000000000000, 0.5000000000000005551 ) ) ;
#2081=EDGE_CURVE ( 'NONE', #4938, #5470, #15859, .T. ) ;
#2122=CARTESIAN_POINT ( 'NONE',  ( 0.7847114317029997288, 2.978485840173427324, -0.8855837454876586134 ) ) ;
#2140=CARTESIAN_POINT ( 'NONE',  ( 2.319244702705235195, 2.291712385858714729, -2.476240473580834323 ) ) ;
#2160=DIRECTION ( 'NONE',  ( -0.000000000000000000, -1.000000000000000000, -0.000000000000000000 ) ) ;
#2162=ADVANCED_FACE ( 'NONE', ( #16101 ), #23515, .T. ) ;
#2173=DIRECTION ( 'NONE',  ( 0.7745966692414850696, -0.4472135954999565954, 0.4472135954999565954 ) ) ;
#2177=FACE_OUTER_BOUND ( 'NONE', #10912, .T. ) ;
#2181=VERTEX_POINT ( 'NONE', #19997 ) ;
#2182=DIRECTION ( 'NONE',  ( -0.8660254037844361541, 0.000000000000000000, -0.5000000000000042188 ) ) ;
#2185=VECTOR ( 'NONE', #10205, 39.37007874015748143 ) ;
#2199=DIRECTION ( 'NONE',  ( -0.000000000000000000, 0.9961946980917454342, -0.08715574274765824914 ) ) ;
#2216=CARTESIAN_POINT ( 'NONE',  ( -1.562282291722813840E-15, 0.000000000000000000, -2.540999999999999037 ) ) ;
#2222=ORIENTED_EDGE ( 'NONE', *, *, #97, .F. ) ;
#2248=ORIENTED_EDGE ( 'NONE', *, *, #11014, .F. ) ;
#2322=CARTESIAN_POINT ( 'NONE',  ( 0.3950000000000000178, 2.740039370078740433, -2.591000000000000192 ) ) ;
#2325=EDGE_LOOP ( 'NONE', ( #2485, #13346, #16518 ) ) ;
#2349=LINE ( 'NONE', #7706, #20263 ) ;
#2362=CARTESIAN_POINT ( 'NONE',  ( 0.000000000000000000, 2.740000000000000213, -0.05000000000000028727 ) ) ;
#2363=ORIENTED_EDGE ( 'NONE', *, *, #14733, .T. ) ;
#2379=CARTESIAN_POINT ( 'NONE',  ( 1.222470958122163998, 2.291712385858715173, -0.8172771125692949168 ) ) ;
#2394=ORIENTED_EDGE ( 'NONE', *, *, #7688, .T. ) ;
#2410=CARTESIAN_POINT ( 'NONE',  ( 1.222470958122163998, 2.978485840173427324, -0.8773620042323713175 ) ) ;
#2415=DIRECTION ( 'NONE',  ( 1.000000000000000000, 0.000000000000000000, 0.000000000000000000 ) ) ;
#2425=DIRECTION ( 'NONE',  ( 0.000000000000000000, 0.000000000000000000, -1.000000000000000000 ) ) ;
#2440=CARTESIAN_POINT ( 'NONE',  ( 0.5097595264191659981, 2.291712385858714729, -0.6667552972947653478 ) ) ;
#2442=FACE_OUTER_BOUND ( 'NONE', #19762, .T. ) ;
#2444=ORIENTED_EDGE ( 'NONE', *, *, #3668, .T. ) ;
#2453=CARTESIAN_POINT ( 'NONE',  ( 1.573500000000000343, 0.000000000000000000, -0.1650000000000001465 ) ) ;
#2466=CARTESIAN_POINT ( 'NONE',  ( 0.000000000000000000, 0.05000000000000028727, -2.986000000000000210 ) ) ;
#2472=EDGE_CURVE ( 'NONE', #22384, #13614, #15475, .T. ) ;
#2485=ORIENTED_EDGE ( 'NONE', *, *, #15981, .F. ) ;
#2500=CIRCLE ( 'NONE', #13795, 0.2124999999999999944 ) ;
#2525=PLANE ( 'NONE',  #15932 ) ;
#2529=CARTESIAN_POINT ( 'NONE',  ( 1.573500000000000343, -3.414809992080329023E-17, -0.1400000000000000133 ) ) ;
#2547=DIRECTION ( 'NONE',  ( 0.000000000000000000, 0.000000000000000000, -1.000000000000000000 ) ) ;
#2548=LINE ( 'NONE', #8502, #22219 ) ;
#2595=ORIENTED_EDGE ( 'NONE', *, *, #8284, .F. ) ;
#2600=ORIENTED_EDGE ( 'NONE', *, *, #11117, .F. ) ;
#2601=EDGE_CURVE ( 'NONE', #6853, #13735, #12070, .T. ) ;
#2602=ADVANCED_FACE ( 'NONE', ( #14121 ), #2628, .F. ) ;
#2607=ORIENTED_EDGE ( 'NONE', *, *, #776, .T. ) ;
#2614=DIRECTION ( 'NONE',  ( 0.7071067811865476838, -0.7071067811865474617, 1.207317650931790858E-16 ) ) ;
#2621=CARTESIAN_POINT ( 'NONE',  ( 0.3950000000000000178, 0.05000000000000028727, -1.966000000000000192 ) ) ;
#2627=EDGE_CURVE ( 'NONE', #8315, #8144, #13936, .T. ) ;
#2628=CONICAL_SURFACE ( 'NONE', #17417, 0.1874999999999998335, 1.029744258676652757 ) ;
#2629=EDGE_LOOP ( 'NONE', ( #2985, #23303, #17357, #22746 ) ) ;
#2631=DIRECTION ( 'NONE',  ( -0.000000000000000000, -1.000000000000000000, -0.000000000000000000 ) ) ;
#2641=ORIENTED_EDGE ( 'NONE', *, *, #3192, .F. ) ;
#2643=DIRECTION ( 'NONE',  ( 0.4999999999999798495, 0.000000000000000000, -0.8660254037844501429 ) ) ;
#2654=EDGE_LOOP ( 'NONE', ( #12891, #3424, #4036, #22897, #22351, #12950 ) ) ;
#2660=EDGE_CURVE ( 'NONE', #7579, #18699, #2777, .T. ) ;
#2665=CARTESIAN_POINT ( 'NONE',  ( 0.8119709581221709049, 2.291712385858714729, -1.528283969076322801 ) ) ;
#2668=EDGE_LOOP ( 'NONE', ( #22740, #19410 ) ) ;
#2670=CARTESIAN_POINT ( 'NONE',  ( 1.573500000000000343, -3.414809992080329023E-17, -1.412500000000000089 ) ) ;
#2679=ORIENTED_EDGE ( 'NONE', *, *, #19446, .T. ) ;
#2680=VECTOR ( 'NONE', #18195, 39.37007874015748854 ) ;
#2681=CARTESIAN_POINT ( 'NONE',  ( 0.1580000000000001403, -0.1079999999999998461, -1.920389328734020129 ) ) ;
#2696=CARTESIAN_POINT ( 'NONE',  ( 1.845714884748260509, 0.000000000000000000, -2.498788568296995916 ) ) ;
#2712=DIRECTION ( 'NONE',  ( -0.4995222938423280468, -0.04370253788966921987, 0.8651979924482607887 ) ) ;
#2715=EDGE_CURVE ( 'NONE', #1184, #11161, #8627, .T. ) ;
#2732=CARTESIAN_POINT ( 'NONE',  ( 1.998815303304993796, 2.291712385858714285, -2.661240473580833488 ) ) ;
#2741=EDGE_CURVE ( 'NONE', #13618, #13239, #8261, .T. ) ;
#2743=VECTOR ( 'NONE', #4670, 39.37007874015748143 ) ;
#2753=LINE ( 'NONE', #19697, #2185 ) ;
#2756=EDGE_LOOP ( 'NONE', ( #11888, #10367 ) ) ;
#2767=EDGE_CURVE ( 'NONE', #22988, #16899, #19073, .T. ) ;
#2772=DIRECTION ( 'NONE',  ( -0.000000000000000000, -1.000000000000000000, -0.000000000000000000 ) ) ;
#2773=ORIENTED_EDGE ( 'NONE', *, *, #10048, .T. ) ;
#2777=LINE ( 'NONE', #10471, #10819 ) ;
#2814=CARTESIAN_POINT ( 'NONE',  ( -0.1319936186941939871, 0.1819936186941943090, -0.5389016700558214579 ) ) ;
#2819=VECTOR ( 'NONE', #22880, 39.37007874015748143 ) ;
#2823=VERTEX_POINT ( 'NONE', #9937 ) ;
#2825=PLANE ( 'NONE',  #6205 ) ;
#2827=DIRECTION ( 'NONE',  ( 0.4999999999999913403, 0.000000000000000000, -0.8660254037844434816 ) ) ;
#2830=AXIS2_PLACEMENT_3D ( 'NONE', #7328, #6846, #14654 ) ;
#2847=CARTESIAN_POINT ( 'NONE',  ( 2.936000000000000387, 0.04999999999999970440, -2.591000000000000636 ) ) ;
#2854=ORIENTED_EDGE ( 'NONE', *, *, #21097, .F. ) ;
#2864=EDGE_LOOP ( 'NONE', ( #15028, #19768, #5292, #18193 ) ) ;
#2868=DIRECTION ( 'NONE',  ( -0.5773502691896257311, -0.5773502691896257311, 0.5773502691896257311 ) ) ;
#2869=EDGE_CURVE ( 'NONE', #20123, #1184, #16017, .T. ) ;
#2874=CARTESIAN_POINT ( 'NONE',  ( 0.4449999999999992295, 3.150471934781994425E-18, -0.04999999999999917705 ) ) ;
#2879=PLANE ( 'NONE',  #14029 ) ;
#2881=AXIS2_PLACEMENT_3D ( 'NONE', #84, #7650, #5814 ) ;
#2898=ORIENTED_EDGE ( 'NONE', *, *, #23620, .T. ) ;
#2901=FACE_OUTER_BOUND ( 'NONE', #21876, .T. ) ;
#2915=EDGE_CURVE ( 'NONE', #23447, #12633, #19670, .T. ) ;
#2922=LINE ( 'NONE', #23509, #16179 ) ;
#2937=DIRECTION ( 'NONE',  ( 0.000000000000000000, -0.7071067811865474617, 0.7071067811865474617 ) ) ;
#2946=LINE ( 'NONE', #12236, #3236 ) ;
#2948=CARTESIAN_POINT ( 'NONE',  ( 2.986000000000000210, 0.05000000000000028727, 0.000000000000000000 ) ) ;
#2956=ORIENTED_EDGE ( 'NONE', *, *, #21533, .T. ) ;
#2961=VERTEX_POINT ( 'NONE', #15778 ) ;
#2979=DIRECTION ( 'NONE',  ( -0.000000000000000000, -1.000000000000000000, -0.000000000000000000 ) ) ;
#2985=ORIENTED_EDGE ( 'NONE', *, *, #13200, .F. ) ;
#2988=ORIENTED_EDGE ( 'NONE', *, *, #12774, .F. ) ;
#2991=CARTESIAN_POINT ( 'NONE',  ( 1.123474536090420584, 2.661358883302036293, -1.021083823334169027 ) ) ;
#2994=VECTOR ( 'NONE', #4397, 39.37007874015748143 ) ;
#3012=VECTOR ( 'NONE', #713, 39.37007874015748143 ) ;
#3013=CARTESIAN_POINT ( 'NONE',  ( 0.3155047199421904813, 2.819495280057808362, -0.1294952800578086372 ) ) ;
#3016=EDGE_CURVE ( 'NONE', #20507, #16517, #23434, .T. ) ;
#3042=EDGE_CURVE ( 'NONE', #4696, #23447, #10424, .T. ) ;
#3053=CARTESIAN_POINT ( 'NONE',  ( 3.799666666666678072, 1.876333333333333631, -1.727333333333314291 ) ) ;
#3059=CARTESIAN_POINT ( 'NONE',  ( 0.4449999999999992295, 0.04999999999999919092, 0.000000000000000000 ) ) ;
#3063=VECTOR ( 'NONE', #7733, 39.37007874015748143 ) ;
#3071=FACE_OUTER_BOUND ( 'NONE', #17815, .T. ) ;
#3085=ORIENTED_EDGE ( 'NONE', *, *, #3366, .T. ) ;
#3095=DIRECTION ( 'NONE',  ( 0.2455557836931403226, -0.6854569122471694254, 0.6854569122471694254 ) ) ;
#3104=ORIENTED_EDGE ( 'NONE', *, *, #3237, .F. ) ;
#3105=EDGE_CURVE ( 'NONE', #8144, #8315, #16645, .T. ) ;
#3108=LINE ( 'NONE', #16404, #14629 ) ;
#3109=CARTESIAN_POINT ( 'NONE',  ( 1.645216030923674522, 2.291712385858714729, -2.498788568296995916 ) ) ;
#3117=DIRECTION ( 'NONE',  ( 0.000000000000000000, 0.000000000000000000, 1.000000000000000000 ) ) ;
#3123=DIRECTION ( 'NONE',  ( -1.000000000000000000, 0.000000000000000000, 0.000000000000000000 ) ) ;
#3131=PLANE ( 'NONE',  #14599 ) ;
#3135=VECTOR ( 'NONE', #23066, 39.37007874015748854 ) ;
#3136=EDGE_CURVE ( 'NONE', #18090, #19497, #8813, .T. ) ;
#3144=CARTESIAN_POINT ( 'NONE',  ( 2.969333333333334490, 2.706666666666668331, -0.05833333333333418080 ) ) ;
#3145=FACE_BOUND ( 'NONE', #2756, .T. ) ;
#3150=DIRECTION ( 'NONE',  ( 0.000000000000000000, 0.000000000000000000, -1.000000000000000000 ) ) ;
#3151=FACE_OUTER_BOUND ( 'NONE', #13925, .T. ) ;
#3172=ORIENTED_EDGE ( 'NONE', *, *, #7936, .T. ) ;
#3179=EDGE_CURVE ( 'NONE', #21850, #23449, #13104, .T. ) ;
#3182=FACE_OUTER_BOUND ( 'NONE', #4475, .T. ) ;
#3192=EDGE_CURVE ( 'NONE', #13735, #7263, #18972, .T. ) ;
#3205=DIRECTION ( 'NONE',  ( -0.000000000000000000, -1.000000000000000000, -0.000000000000000000 ) ) ;
#3219=AXIS2_PLACEMENT_3D ( 'NONE', #13395, #11567, #3123 ) ;
#3236=VECTOR ( 'NONE', #1118, 39.37007874015748854 ) ;
#3237=EDGE_CURVE ( 'NONE', #8054, #8072, #7415, .T. ) ;
#3240=DIRECTION ( 'NONE',  ( 8.659560562354932858E-17, 0.7071067811865474617, -0.7071067811865474617 ) ) ;
#3248=VECTOR ( 'NONE', #10828, 39.37007874015748854 ) ;
#3281=CARTESIAN_POINT ( 'NONE',  ( 0.4235215514428773420, 2.693521551442877193, -0.6521195261172616497 ) ) ;
#3297=PRODUCT_DEFINITION_SHAPE ( 'NONE', 'NONE',  #21185 ) ;
#3298=FACE_OUTER_BOUND ( 'NONE', #6519, .T. ) ;
#3312=CARTESIAN_POINT ( 'NONE',  ( 2.320391506243691726, 2.740000000000000213, -2.452934640057647719 ) ) ;
#3317=DIRECTION ( 'NONE',  ( 0.8660254037844361541, 0.000000000000000000, 0.5000000000000042188 ) ) ;
#3318=AXIS2_PLACEMENT_3D ( 'NONE', #13654, #20832, #2425 ) ;
#3325=PLANE ( 'NONE',  #8132 ) ;
#3360=EDGE_CURVE ( 'NONE', #2823, #10167, #1921, .T. ) ;
#3366=EDGE_CURVE ( 'NONE', #7614, #17116, #13459, .T. ) ;
#3367=ADVANCED_FACE ( 'NONE', ( #20700 ), #15337, .F. ) ;
#3370=ORIENTED_EDGE ( 'NONE', *, *, #7090, .T. ) ;
#3372=EDGE_CURVE ( 'NONE', #19011, #4071, #18995, .T. ) ;
#3376=LINE ( 'NONE', #21906, #3248 ) ;
#3396=ORIENTED_EDGE ( 'NONE', *, *, #23175, .T. ) ;
#3415=ORIENTED_EDGE ( 'NONE', *, *, #5906, .F. ) ;
#3424=ORIENTED_EDGE ( 'NONE', *, *, #2601, .T. ) ;
#3469=LINE ( 'NONE', #12764, #17579 ) ;
#3471=CARTESIAN_POINT ( 'NONE',  ( 0.4700000000000001954, 2.740000000000000213, -2.516000000000000014 ) ) ;
#3472=DIRECTION ( 'NONE',  ( -0.000000000000000000, -1.000000000000000000, -0.000000000000000000 ) ) ;
#3473=VERTEX_POINT ( 'NONE', #332 ) ;
#3487=CARTESIAN_POINT ( 'NONE',  ( 1.957333333333323822, 3.718666666666667009, -1.537333333333325669 ) ) ;
#3489=VECTOR ( 'NONE', #398, 39.37007874015748143 ) ;
#3494=DIRECTION ( 'NONE',  ( -1.000000000000000000, 0.000000000000000000, 6.148297094540788948E-16 ) ) ;
#3496=DIRECTION ( 'NONE',  ( 0.8660254037844455910, -0.000000000000000000, -0.4999999999999880096 ) ) ;
#3501=CARTESIAN_POINT ( 'NONE',  ( 0.7847114317029997288, 0.000000000000000000, -0.6249999999999962252 ) ) ;
#3505=CARTESIAN_POINT ( 'NONE',  ( 1.222470958122163998, 0.000000000000000000, -0.6167782587447089293 ) ) ;
#3506=VECTOR ( 'NONE', #13354, 39.37007874015748854 ) ;
#3521=DIRECTION ( 'NONE',  ( 0.5000000000000007772, 0.000000000000000000, 0.8660254037844382635 ) ) ;
#3578=ORIENTED_EDGE ( 'NONE', *, *, #10217, .F. ) ;
#3579=EDGE_LOOP ( 'NONE', ( #1592, #5114, #11152, #15673 ) ) ;
#3586=LINE ( 'NONE', #3953, #10138 ) ;
#3594=LINE ( 'NONE', #20068, #19681 ) ;
#3602=AXIS2_PLACEMENT_3D ( 'NONE', #8745, #21683, #1076 ) ;
#3615=CARTESIAN_POINT ( 'NONE',  ( 1.585131139260598010, 2.978485840173427324, -2.498788568296995916 ) ) ;
#3629=CARTESIAN_POINT ( 'NONE',  ( 0.000000000000000000, 2.689999999999999947, -2.165185842870423816 ) ) ;
#3635=ORIENTED_EDGE ( 'NONE', *, *, #8017, .F. ) ;
#3650=CARTESIAN_POINT ( 'NONE',  ( 0.8119709581221709049, 0.000000000000000000, -1.327785115251736814 ) ) ;
#3652=VECTOR ( 'NONE', #18771, 39.37007874015748143 ) ;
#3663=CARTESIAN_POINT ( 'NONE',  ( 0.000000000000000000, 2.777857142857143913, -2.063737152712815881 ) ) ;
#3668=EDGE_CURVE ( 'NONE', #15698, #11818, #15573, .T. ) ;
#3676=DIRECTION ( 'NONE',  ( -1.000000000000000000, 0.000000000000000000, -0.000000000000000000 ) ) ;
#3697=DIRECTION ( 'NONE',  ( 1.000000000000000000, 0.000000000000000000, 0.000000000000000000 ) ) ;
#3712=ORIENTED_EDGE ( 'NONE', *, *, #7688, .F. ) ;
#3727=LINE ( 'NONE', #16419, #7894 ) ;
#3728=CARTESIAN_POINT ( 'NONE',  ( 0.3950000000000000733, 2.978485840173427324, -0.6605837454876625214 ) ) ;
#3738=ORIENTED_EDGE ( 'NONE', *, *, #7836, .T. ) ;
#3743=DIRECTION ( 'NONE',  ( 1.000000000000000000, 0.000000000000000000, -0.000000000000000000 ) ) ;
#3752=EDGE_CURVE ( 'NONE', #10167, #13618, #14222, .T. ) ;
#3753=DIRECTION ( 'NONE',  ( 0.8660254037844431485, 0.000000000000000000, 0.4999999999999918954 ) ) ;
#3756=CARTESIAN_POINT ( 'NONE',  ( 1.829696540937382654, 2.476534978792082065, -1.949930308767543030 ) ) ;
#3763=VECTOR ( 'NONE', #14700, 39.37007874015748143 ) ;
#3770=DIRECTION ( 'NONE',  ( 0.000000000000000000, 0.000000000000000000, -1.000000000000000000 ) ) ;
#3779=CARTESIAN_POINT ( 'NONE',  ( 0.03174294256098306871, 0.01825705743901666692, -0.6191099248581333203 ) ) ;
#3791=ADVANCED_FACE ( 'NONE', ( #23469 ), #1054, .T. ) ;
#3794=CARTESIAN_POINT ( 'NONE',  ( 2.285102959650015197, 2.697839921951305175, -2.464255729834791797 ) ) ;
#3799=LINE ( 'NONE', #1970, #15615 ) ;
#3802=EDGE_LOOP ( 'NONE', ( #2222, #17313, #22434, #23234 ) ) ;
#3812=CARTESIAN_POINT ( 'NONE',  ( 1.095241930731965629, 2.405295409249399441, -1.047581479122380754 ) ) ;
#3816=VECTOR ( 'NONE', #13139, 39.37007874015748143 ) ;
#3820=DIRECTION ( 'NONE',  ( -0.7071067811865475727, -0.000000000000000000, -0.7071067811865475727 ) ) ;
#3824=EDGE_CURVE ( 'NONE', #10167, #14330, #20073, .T. ) ;
#3828=AXIS2_PLACEMENT_3D ( 'NONE', #10600, #5091, #8386 ) ;
#3829=ORIENTED_EDGE ( 'NONE', *, *, #10998, .F. ) ;
#3831=LINE ( 'NONE', #1876, #3763 ) ;
#3864=VECTOR ( 'NONE', #2643, 39.37007874015748854 ) ;
#3875=CARTESIAN_POINT ( 'NONE',  ( 1.573500000000000343, -3.414809992080329023E-17, -0.3524999999999999800 ) ) ;
#3881=LINE ( 'NONE', #20705, #16782 ) ;
#3887=CARTESIAN_POINT ( 'NONE',  ( 1.222470958122163998, 0.000000000000000000, -0.6167782587447089293 ) ) ;
#3906=DIRECTION ( 'NONE',  ( 0.000000000000000000, 0.000000000000000000, -1.000000000000000000 ) ) ;
#3908=ORIENTED_EDGE ( 'NONE', *, *, #15981, .T. ) ;
#3913=VECTOR ( 'NONE', #9263, 39.37007874015748143 ) ;
#3915=DIRECTION ( 'NONE',  ( 0.000000000000000000, 0.000000000000000000, -1.000000000000000000 ) ) ;
#3931=DIRECTION ( 'NONE',  ( 0.8660254037844364872, 0.000000000000000000, -0.5000000000000038858 ) ) ;
#3946=EDGE_CURVE ( 'NONE', #21142, #10130, #17137, .T. ) ;
#3948=CARTESIAN_POINT ( 'NONE',  ( 2.283224615330811780, 2.690142902515283208, -2.474227944919804578 ) ) ;
#3952=ORIENTED_EDGE ( 'NONE', *, *, #16480, .T. ) ;
#3953=CARTESIAN_POINT ( 'NONE',  ( 2.361000000000004206, 0.000000000000000000, -2.201288568297000925 ) ) ;
#3954=DIRECTION ( 'NONE',  ( -0.8660254037844360431, 0.000000000000000000, -0.5000000000000043299 ) ) ;
#3957=EDGE_CURVE ( 'NONE', #6883, #2823, #8305, .T. ) ;
#3972=ORIENTED_EDGE ( 'NONE', *, *, #10217, .T. ) ;
#3985=VECTOR ( 'NONE', #3240, 39.37007874015748854 ) ;
#3993=LINE ( 'NONE', #23081, #24091 ) ;
#3998=( BOUNDED_SURFACE ( )  B_SPLINE_SURFACE ( 3, 1, ( 
 ( #12143, #21144 ),
 ( #14072, #1143 ),
 ( #8580, #6746 ),
 ( #23077, #2732 ) ),
 .UNSPECIFIED., .F., .F., .F. ) 
 B_SPLINE_SURFACE_WITH_KNOTS ( ( 4, 4 ),
 ( 2, 2 ),
 ( 0.000000000000000000, 1.000000000000000000 ),
 ( 0.000000000000000000, 1.000000000000000000 ),
 .UNSPECIFIED. ) 
 GEOMETRIC_REPRESENTATION_ITEM ( )  RATIONAL_B_SPLINE_SURFACE ( (
 ( 1.000000000000000000, 1.000000000000000000),
 ( 0.3333333333333338144, 0.3333333333333338144),
 ( 0.3333333333333338144, 0.3333333333333338144),
 ( 1.000000000000000000, 1.000000000000000000) ) ) 
 REPRESENTATION_ITEM ( '' )  SURFACE ( )  );
#4008=ADVANCED_FACE ( 'NONE', ( #5790, #13254 ), #11175, .F. ) ;
#4024=ORIENTED_EDGE ( 'NONE', *, *, #22145, .T. ) ;
#4036=ORIENTED_EDGE ( 'NONE', *, *, #3192, .T. ) ;
#4043=FACE_OUTER_BOUND ( 'NONE', #17823, .T. ) ;
#4051=DIRECTION ( 'NONE',  ( 0.000000000000000000, 0.000000000000000000, -1.000000000000000000 ) ) ;
#4055=LINE ( 'NONE', #18815, #14983 ) ;
#4060=DIRECTION ( 'NONE',  ( 1.000000000000000000, 0.000000000000000000, -0.000000000000000000 ) ) ;
#4071=VERTEX_POINT ( 'NONE', #9576 ) ;
#4082=ORIENTED_EDGE ( 'NONE', *, *, #22697, .T. ) ;
#4087=EDGE_LOOP ( 'NONE', ( #3829, #12086, #1304, #10874, #7225, #836 ) ) ;
#4090=DIRECTION ( 'NONE',  ( -0.8660254037844383745, 0.000000000000000000, -0.5000000000000004441 ) ) ;
#4107=CARTESIAN_POINT ( 'NONE',  ( 0.7919466436700954848, 0.05000000000000028727, -2.986000000000000210 ) ) ;
#4123=CARTESIAN_POINT ( 'NONE',  ( 2.160501146175418441, 2.291712385858714285, -2.201288568297000481 ) ) ;
#4144=ADVANCED_FACE ( 'NONE', ( #3298 ), #10752, .F. ) ;
#4152=VECTOR ( 'NONE', #15002, 39.37007874015748143 ) ;
#4178=ORIENTED_EDGE ( 'NONE', *, *, #19169, .F. ) ;
#4188=AXIS2_PLACEMENT_3D ( 'NONE', #7563, #13194, #3906 ) ;
#4194=ORIENTED_EDGE ( 'NONE', *, *, #18397, .F. ) ;
#4220=AXIS2_PLACEMENT_3D ( 'NONE', #5658, #13122, #23813 ) ;
#4236=ORIENTED_EDGE ( 'NONE', *, *, #13057, .F. ) ;
#4242=ADVANCED_FACE ( 'NONE', ( #18539 ), #1952, .F. ) ;
#4247=ORIENTED_EDGE ( 'NONE', *, *, #21838, .F. ) ;
#4266=ORIENTED_EDGE ( 'NONE', *, *, #18875, .F. ) ;
#4276=DIRECTION ( 'NONE',  ( 0.7559289460184540621, 0.6546536707079775308, -0.000000000000000000 ) ) ;
#4291=DIRECTION ( 'NONE',  ( 0.000000000000000000, -0.5249267702233982869, 0.8511473937590547933 ) ) ;
#4292=VECTOR ( 'NONE', #8249, 39.37007874015748143 ) ;
#4297=CARTESIAN_POINT ( 'NONE',  ( 0.4324999999999994404, 2.702499999999999236, -0.01249999999999974742 ) ) ;
#4298=ORIENTED_EDGE ( 'NONE', *, *, #21779, .F. ) ;
#4300=VECTOR ( 'NONE', #3095, 39.37007874015748854 ) ;
#4305=EDGE_LOOP ( 'NONE', ( #11897, #7458, #22151, #8038, #14062 ) ) ;
#4311=EDGE_CURVE ( 'NONE', #1032, #7960, #18223, .T. ) ;
#4314=DIRECTION ( 'NONE',  ( 0.4999999999999913403, -0.000000000000000000, 0.8660254037844434816 ) ) ;
#4340=EDGE_LOOP ( 'NONE', ( #15670, #16425, #4266, #1598, #3172 ) ) ;
#4347=DIRECTION ( 'NONE',  ( 0.4995222938423279913, 0.04370253788966922681, -0.8651979924482608997 ) ) ;
#4367=DIRECTION ( 'NONE',  ( -0.4995222938423278802, -0.04370253788966928232, 0.8651979924482610107 ) ) ;
#4371=CARTESIAN_POINT ( 'NONE',  ( 0.5097595264191663311, 2.319533376497111554, -0.6691893185836859104 ) ) ;
#4387=ADVANCED_FACE ( 'NONE', ( #9637 ), #16947, .T. ) ;
#4397=DIRECTION ( 'NONE',  ( 0.4999999999999912292, 0.000000000000000000, -0.8660254037844437036 ) ) ;
#4429=CARTESIAN_POINT ( 'NONE',  ( 0.3950000000000000178, 2.665000000000000036, -0.2605837454876624437 ) ) ;
#4441=ORIENTED_EDGE ( 'NONE', *, *, #15409, .F. ) ;
#4446=ORIENTED_EDGE ( 'NONE', *, *, #22382, .F. ) ;
#4470=VECTOR ( 'NONE', #21337, 39.37007874015748143 ) ;
#4474=FACE_OUTER_BOUND ( 'NONE', #7093, .T. ) ;
#4475=EDGE_LOOP ( 'NONE', ( #22864, #15264, #2600, #6507, #10436, #10846 ) ) ;
#4491=LINE ( 'NONE', #837, #16901 ) ;
#4501=CARTESIAN_POINT ( 'NONE',  ( 0.000000000000000000, 2.662805069640206135, -0.8823420915204682746 ) ) ;
#4502=ORIENTED_EDGE ( 'NONE', *, *, #14381, .T. ) ;
#4521=CARTESIAN_POINT ( 'NONE',  ( 1.658214884748263618, 0.000000000000000000, -2.174029041877829638 ) ) ;
#4526=DIRECTION ( 'NONE',  ( 0.000000000000000000, -0.7071067811865475727, -0.7071067811865475727 ) ) ;
#4527=CARTESIAN_POINT ( 'NONE',  ( 1.106602540378444965, 0.000000000000000000, -2.540999999999999925 ) ) ;
#4544=ADVANCED_FACE ( 'NONE', ( #7802 ), #5964, .T. ) ;
#4557=CARTESIAN_POINT ( 'NONE',  ( 1.573500000000000343, 2.683750000000000746, -1.818749999999999645 ) ) ;
#4566=ORIENTED_EDGE ( 'NONE', *, *, #1736, .T. ) ;
#4570=EDGE_CURVE ( 'NONE', #9859, #1154, #23136, .T. ) ;
#4576=LINE ( 'NONE', #17269, #6941 ) ;
#4582=DIRECTION ( 'NONE',  ( -0.000000000000000000, -0.9961946980917454342, 0.08715574274765830465 ) ) ;
#4594=AXIS2_PLACEMENT_3D ( 'NONE', #9883, #13553, #8152 ) ;
#4609=DIRECTION ( 'NONE',  ( -1.000000000000000000, 0.000000000000000000, 6.148297094540788948E-16 ) ) ;
#4614=LINE ( 'NONE', #476, #8256 ) ;
#4631=DIRECTION ( 'NONE',  ( 0.8660254037844434816, -0.000000000000000000, -0.4999999999999913403 ) ) ;
#4650=DIRECTION ( 'NONE',  ( -0.5000000000000037748, 0.000000000000000000, -0.8660254037844362651 ) ) ;
#4653=CARTESIAN_POINT ( 'NONE',  ( 1.573500000000000343, 0.02500000000000021302, -0.1650000000000001465 ) ) ;
#4655=ADVANCED_FACE ( 'NONE', ( #1326 ), #8513, .T. ) ;
#4656=DIRECTION ( 'NONE',  ( 1.000000000000000000, 0.000000000000000000, 0.000000000000000000 ) ) ;
#4658=EDGE_CURVE ( 'NONE', #19257, #18090, #6566, .T. ) ;
#4667=ORIENTED_EDGE ( 'NONE', *, *, #6146, .T. ) ;
#4670=DIRECTION ( 'NONE',  ( -9.239214857301838159E-19, -0.9961946980917454342, 0.08715574274765830465 ) ) ;
#4673=VECTOR ( 'NONE', #10384, 39.37007874015748854 ) ;
#4674=CARTESIAN_POINT ( 'NONE',  ( 0.2235833740012116433, -0.1735833740012113768, -0.4097528311786164390 ) ) ;
#4685=ADVANCED_FACE ( 'NONE', ( #12320 ), #8751, .T. ) ;
#4686=VECTOR ( 'NONE', #3753, 39.37007874015748854 ) ;
#4690=DIRECTION ( 'NONE',  ( 0.8233282866803208755, -0.5459676143495163503, -0.1550802902806971972 ) ) ;
#4695=CARTESIAN_POINT ( 'NONE',  ( 0.7188945565055682163, 2.836044817640776206, -0.6580815178912685637 ) ) ;
#4696=VERTEX_POINT ( 'NONE', #10482 ) ;
#4704=CARTESIAN_POINT ( 'NONE',  ( 1.573500000000000343, -3.414809992080329023E-17, -0.5649999999999999467 ) ) ;
#4721=CARTESIAN_POINT ( 'NONE',  ( 0.4449999999999992850, 0.000000000000000000, -0.4000000000000000222 ) ) ;
#4724=EDGE_LOOP ( 'NONE', ( #14736, #22960, #21011, #14180 ) ) ;
#4739=EDGE_CURVE ( 'NONE', #13614, #20425, #14016, .T. ) ;
#4762=CONICAL_SURFACE ( 'NONE', #3602, 0.2124999999999999944, 0.7853981633974463916 ) ;
#4776=ORIENTED_EDGE ( 'NONE', *, *, #16978, .F. ) ;
#4777=VECTOR ( 'NONE', #14074, 39.37007874015748143 ) ;
#4805=CARTESIAN_POINT ( 'NONE',  ( 1.573500000000000343, 0.000000000000000000, -1.412500000000000089 ) ) ;
#4808=DIRECTION ( 'NONE',  ( -0.4999999999999918954, -0.000000000000000000, -0.8660254037844431485 ) ) ;
#4811=CARTESIAN_POINT ( 'NONE',  ( 0.7847114317029997288, 2.978485840173427324, -0.8855837454876586134 ) ) ;
#4823=ADVANCED_FACE ( 'NONE', ( #3151 ), #17670, .F. ) ;
#4826=LINE ( 'NONE', #19710, #5836 ) ;
#4827=ORIENTED_EDGE ( 'NONE', *, *, #5893, .F. ) ;
#4828=AXIS2_PLACEMENT_3D ( 'NONE', #13707, #2712, #12126 ) ;
#4847=PLANE ( 'NONE',  #20348 ) ;
#4869=CARTESIAN_POINT ( 'NONE',  ( 0.3950000000000000733, 2.978485840173427324, -0.6605837454876625214 ) ) ;
#4886=EDGE_CURVE ( 'NONE', #12390, #1032, #22529, .T. ) ;
#4890=ADVANCED_FACE ( 'NONE', ( #20944 ), #17287, .T. ) ;
#4898=CONICAL_SURFACE ( 'NONE', #8014, 0.4625000000000000777, 0.7853981633974498333 ) ;
#4901=ORIENTED_EDGE ( 'NONE', *, *, #9910, .F. ) ;
#4909=CARTESIAN_POINT ( 'NONE',  ( 2.325416254512337577, 2.978485840173427324, -2.591000000000000636 ) ) ;
#4922=DIRECTION ( 'NONE',  ( -0.4999999999999918954, -0.000000000000000000, -0.8660254037844432595 ) ) ;
#4938=VERTEX_POINT ( 'NONE', #6181 ) ;
#4970=CARTESIAN_POINT ( 'NONE',  ( 0.000000000000000000, 2.740000000000000213, 0.000000000000000000 ) ) ;
#4982=DIRECTION ( 'NONE',  ( 0.000000000000000000, 0.000000000000000000, -1.000000000000000000 ) ) ;
#5030=DIRECTION ( 'NONE',  ( -0.8660254037844501429, -0.000000000000000000, 0.4999999999999801270 ) ) ;
#5047=DIRECTION ( 'NONE',  ( 0.4999999999999913403, 0.000000000000000000, -0.8660254037844437036 ) ) ;
#5050=VECTOR ( 'NONE', #9661, 39.37007874015748143 ) ;
#5056=CARTESIAN_POINT ( 'NONE',  ( 0.05000000000000028727, 0.000000000000000000, -2.107450815951460221 ) ) ;
#5085=LINE ( 'NONE', #7054, #18783 ) ;
#5091=DIRECTION ( 'NONE',  ( 0.000000000000000000, -0.000000000000000000, 1.000000000000000000 ) ) ;
#5101=CARTESIAN_POINT ( 'NONE',  ( 0.4172595264191667486, 2.291712385858714285, -0.8269699969948853813 ) ) ;
#5114=ORIENTED_EDGE ( 'NONE', *, *, #18843, .F. ) ;
#5125=LINE ( 'NONE', #5493, #23841 ) ;
#5126=ORIENTED_EDGE ( 'NONE', *, *, #1557, .F. ) ;
#5127=CARTESIAN_POINT ( 'NONE',  ( 0.8119709581221709049, 0.000000000000000000, -1.327785115251736814 ) ) ;
#5133=LINE ( 'NONE', #23897, #18923 ) ;
#5136=VERTEX_POINT ( 'NONE', #7847 ) ;
#5137=CARTESIAN_POINT ( 'NONE',  ( 1.573500000000000343, 0.05625000000000004996, -1.006250000000000311 ) ) ;
#5166=VECTOR ( 'NONE', #17485, 39.37007874015748143 ) ;
#5173=FACE_OUTER_BOUND ( 'NONE', #21031, .T. ) ;
#5188=EDGE_CURVE ( 'NONE', #21090, #23820, #4576, .T. ) ;
#5216=EDGE_CURVE ( 'NONE', #11779, #6253, #10850, .T. ) ;
#5223=CIRCLE ( 'NONE', #4828, 0.1850000000000000533 ) ;
#5235=ORIENTED_EDGE ( 'NONE', *, *, #14733, .F. ) ;
#5237=DIRECTION ( 'NONE',  ( 0.000000000000000000, 0.000000000000000000, -1.000000000000000000 ) ) ;
#5243=ORIENTED_EDGE ( 'NONE', *, *, #89, .F. ) ;
#5260=ORIENTED_EDGE ( 'NONE', *, *, #7391, .T. ) ;
#5266=VECTOR ( 'NONE', #1523, 39.37007874015748143 ) ;
#5292=ORIENTED_EDGE ( 'NONE', *, *, #23306, .T. ) ;
#5296=LINE ( 'NONE', #21761, #5266 ) ;
#5305=ADVANCED_FACE ( 'NONE', ( #22978 ), #15992, .F. ) ;
#5306=ORIENTED_EDGE ( 'NONE', *, *, #13032, .F. ) ;
#5318=LINE ( 'NONE', #3487, #8577 ) ;
#5342=CARTESIAN_POINT ( 'NONE',  ( 0.000000000000000000, 2.740039370078740433, -2.194053356329904947 ) ) ;
#5343=ORIENTED_EDGE ( 'NONE', *, *, #20351, .T. ) ;
#5372=VECTOR ( 'NONE', #12083, 39.37007874015748143 ) ;
#5382=DIRECTION ( 'NONE',  ( 0.000000000000000000, 0.000000000000000000, -1.000000000000000000 ) ) ;
#5386=EDGE_LOOP ( 'NONE', ( #16208, #548, #5901, #12355 ) ) ;
#5389=DIRECTION ( 'NONE',  ( -0.3993784937532310342, 0.7060941387255963431, 0.5847460012558945985 ) ) ;
#5401=EDGE_CURVE ( 'NONE', #16274, #22355, #21516, .T. ) ;
#5403=FACE_OUTER_BOUND ( 'NONE', #14083, .T. ) ;
#5408=VECTOR ( 'NONE', #5506, 39.37007874015748143 ) ;
#5411=ORIENTED_EDGE ( 'NONE', *, *, #16172, .T. ) ;
#5422=DIRECTION ( 'NONE',  ( -0.8660254037844523634, -0.000000000000000000, 0.4999999999999761857 ) ) ;
#5439=EDGE_LOOP ( 'NONE', ( #14167, #19202, #19957, #12761 ) ) ;
#5440=EDGE_CURVE ( 'NONE', #17116, #16274, #14089, .T. ) ;
#5443=ORIENTED_EDGE ( 'NONE', *, *, #830, .F. ) ;
#5457=EDGE_CURVE ( 'NONE', #19011, #11232, #21879, .T. ) ;
#5462=VECTOR ( 'NONE', #21473, 39.37007874015748143 ) ;
#5470=VERTEX_POINT ( 'NONE', #17990 ) ;
#5486=ORIENTED_EDGE ( 'NONE', *, *, #7333, .T. ) ;
#5493=CARTESIAN_POINT ( 'NONE',  ( 2.007333333333344516, 1.736333333333339501, -3.519666666666666721 ) ) ;
#5502=CARTESIAN_POINT ( 'NONE',  ( 0.8785491840485403214, 0.000000000000000000, -2.935999999999999943 ) ) ;
#5506=DIRECTION ( 'NONE',  ( -0.4999999999999913403, 0.000000000000000000, 0.8660254037844437036 ) ) ;
#5512=CARTESIAN_POINT ( 'NONE',  ( 0.3950000000000000178, 0.05000000000000028727, -1.966000000000000192 ) ) ;
#5531=ORIENTED_EDGE ( 'NONE', *, *, #2741, .T. ) ;
#5560=ORIENTED_EDGE ( 'NONE', *, *, #18132, .T. ) ;
#5573=EDGE_CURVE ( 'NONE', #19216, #4938, #20298, .T. ) ;
#5576=CARTESIAN_POINT ( 'NONE',  ( 1.573500000000000343, 0.5250000000000000222, -0.5399999999999998135 ) ) ;
#5577=LINE ( 'NONE', #16562, #6719 ) ;
#5598=LINE ( 'NONE', #3650, #13658 ) ;
#5601=ADVANCED_FACE ( 'NONE', ( #14702 ), #11273, .T. ) ;
#5602=ORIENTED_EDGE ( 'NONE', *, *, #18365, .T. ) ;
#5612=ORIENTED_EDGE ( 'NONE', *, *, #18696, .T. ) ;
#5627=ORIENTED_EDGE ( 'NONE', *, *, #12539, .T. ) ;
#5652=EDGE_LOOP ( 'NONE', ( #13403, #22438, #12834, #21050 ) ) ;
#5658=CARTESIAN_POINT ( 'NONE',  ( 1.020000000000000018, 2.665000000000000036, -2.591000000000000192 ) ) ;
#5661=VERTEX_POINT ( 'NONE', #18704 ) ;
#5674=CARTESIAN_POINT ( 'NONE',  ( 1.020000000000000018, 0.000000000000000000, -2.540999999999999925 ) ) ;
#5687=FACE_OUTER_BOUND ( 'NONE', #4305, .T. ) ;
#5701=DIRECTION ( 'NONE',  ( -0.000000000000000000, -1.000000000000000000, -0.000000000000000000 ) ) ;
#5702=CARTESIAN_POINT ( 'NONE',  ( 2.064333333333333353, 0.8966666666666665009, 0.8466666666666669006 ) ) ;
#5703=ADVANCED_FACE ( 'NONE', ( #1878 ), #14575, .F. ) ;
#5706=CARTESIAN_POINT ( 'NONE',  ( 1.573500000000000343, -3.414809992080329023E-17, -1.412500000000000089 ) ) ;
#5715=CARTESIAN_POINT ( 'NONE',  ( 2.725416254512337932, 2.978485840173427324, -2.591000000000000636 ) ) ;
#5742=AXIS2_PLACEMENT_3D ( 'NONE', #17970, #3205, #1383 ) ;
#5751=ORIENTED_EDGE ( 'NONE', *, *, #12124, .T. ) ;
#5761=CARTESIAN_POINT ( 'NONE',  ( 1.079423153357894183, 2.439495096761426396, -1.077972490201325906 ) ) ;
#5773=VECTOR ( 'NONE', #9489, 39.37007874015748143 ) ;
#5775=CARTESIAN_POINT ( 'NONE',  ( 1.972716373660570399, 2.672602470488781190, -2.673753908138122526 ) ) ;
#5781=FACE_OUTER_BOUND ( 'NONE', #15701, .T. ) ;
#5784=ORIENTED_EDGE ( 'NONE', *, *, #20361, .T. ) ;
#5786=LINE ( 'NONE', #11528, #1776 ) ;
#5790=FACE_BOUND ( 'NONE', #2668, .T. ) ;
#5792=AXIS2_PLACEMENT_3D ( 'NONE', #21374, #12133, #1009 ) ;
#5797=VERTEX_POINT ( 'NONE', #19421 ) ;
#5814=DIRECTION ( 'NONE',  ( 0.8660254037844361541, 0.000000000000000000, 0.5000000000000042188 ) ) ;
#5820=PLANE ( 'NONE',  #6186 ) ;
#5823=DIRECTION ( 'NONE',  ( 0.5589148618992055839, 0.8148277346686835232, -0.1538503817443866439 ) ) ;
#5832=ORIENTED_EDGE ( 'NONE', *, *, #21809, .F. ) ;
#5834=ADVANCED_FACE ( 'NONE', ( #21491 ), #886, .T. ) ;
#5836=VECTOR ( 'NONE', #10461, 39.37007874015748143 ) ;
#5842=LINE ( 'NONE', #13305, #537 ) ;
#5851=EDGE_LOOP ( 'NONE', ( #13655, #10913, #18380, #20492 ) ) ;
#5883=ORIENTED_EDGE ( 'NONE', *, *, #3136, .T. ) ;
#5889=ADVANCED_FACE ( 'NONE', ( #10172 ), #13944, .F. ) ;
#5893=EDGE_CURVE ( 'NONE', #20052, #21090, #8439, .T. ) ;
#5894=ADVANCED_FACE ( 'NONE', ( #11004 ), #1490, .F. ) ;
#5901=ORIENTED_EDGE ( 'NONE', *, *, #15732, .F. ) ;
#5903=VERTEX_POINT ( 'NONE', #7577 ) ;
#5906=EDGE_CURVE ( 'NONE', #544, #21142, #10769, .T. ) ;
#5908=CARTESIAN_POINT ( 'NONE',  ( 2.936000000000000387, 0.000000000000000000, -0.04999999999999918399 ) ) ;
#5931=DIRECTION ( 'NONE',  ( -0.3535533905932684018, -0.7071067811865462405, -0.6123724356957992443 ) ) ;
#5937=PLANE ( 'NONE',  #3219 ) ;
#5947=CONICAL_SURFACE ( 'NONE', #17633, 0.1874999999999998335, 1.029744258676652757 ) ;
#5955=DIRECTION ( 'NONE',  ( -0.5773502691896299499, 0.5773502691896236216, -0.5773502691896236216 ) ) ;
#5964=PLANE ( 'NONE',  #6538 ) ;
#5975=CARTESIAN_POINT ( 'NONE',  ( 2.325416254512337577, 2.978485840173427324, -2.591000000000000636 ) ) ;
#5978=VECTOR ( 'NONE', #13101, 39.37007874015748143 ) ;
#5989=LINE ( 'NONE', #504, #5050 ) ;
#6019=FACE_OUTER_BOUND ( 'NONE', #2864, .T. ) ;
#6028=ORIENTED_EDGE ( 'NONE', *, *, #3668, .F. ) ;
#6030=ADVANCED_FACE ( 'NONE', ( #16847 ), #16727, .F. ) ;
#6032=EDGE_CURVE ( 'NONE', #10685, #11161, #12603, .T. ) ;
#6040=CARTESIAN_POINT ( 'NONE',  ( 1.109470958122167561, 2.291712385858714285, -1.012998853824579992 ) ) ;
#6071=DIRECTION ( 'NONE',  ( 0.7071067811865475727, 1.056266077312805546E-17, -0.7071067811865475727 ) ) ;
#6081=DIRECTION ( 'NONE',  ( -0.8660254037844434816, 0.000000000000000000, 0.4999999999999914513 ) ) ;
#6085=VECTOR ( 'NONE', #10019, 39.37007874015748143 ) ;
#6088=DIRECTION ( 'NONE',  ( 0.5000000000000007772, 0.000000000000000000, 0.8660254037844382635 ) ) ;
#6097=AXIS2_PLACEMENT_3D ( 'NONE', #14548, #21972, #20150 ) ;
#6109=PLANE ( 'NONE',  #396 ) ;
#6118=VECTOR ( 'NONE', #11441, 39.37007874015748854 ) ;
#6123=FACE_OUTER_BOUND ( 'NONE', #17004, .T. ) ;
#6126=LINE ( 'NONE', #11885, #10553 ) ;
#6128=ORIENTED_EDGE ( 'NONE', *, *, #11014, .T. ) ;
#6146=EDGE_CURVE ( 'NONE', #10162, #22655, #6223, .T. ) ;
#6154=VERTEX_POINT ( 'NONE', #8168 ) ;
#6165=VECTOR ( 'NONE', #6287, 39.37007874015748854 ) ;
#6181=CARTESIAN_POINT ( 'NONE',  ( 2.986000000000000210, 2.690000000000002167, -2.541000000000000369 ) ) ;
#6183=CARTESIAN_POINT ( 'NONE',  ( 0.3247595264191652786, 2.685901063997345961, -1.021671737322407791 ) ) ;
#6184=ORIENTED_EDGE ( 'NONE', *, *, #14253, .T. ) ;
#6186=AXIS2_PLACEMENT_3D ( 'NONE', #10064, #9369, #18878 ) ;
#6201=LINE ( 'NONE', #11829, #21812 ) ;
#6205=AXIS2_PLACEMENT_3D ( 'NONE', #2948, #10282, #10406 ) ;
#6218=DIRECTION ( 'NONE',  ( 1.000000000000000000, 0.000000000000000000, -6.148297094540788948E-16 ) ) ;
#6219=ADVANCED_BREP_SHAPE_REPRESENTATION ( '', ( #9145, #9127 ), #558 ) ;
#6223=LINE ( 'NONE', #13571, #18252 ) ;
#6226=LINE ( 'NONE', #7701, #2994 ) ;
#6239=LINE ( 'NONE', #1990, #8279 ) ;
#6249=ORIENTED_EDGE ( 'NONE', *, *, #16291, .F. ) ;
#6253=VERTEX_POINT ( 'NONE', #9257 ) ;
#6260=DIRECTION ( 'NONE',  ( -0.7071067811865474617, 0.000000000000000000, 0.7071067811865474617 ) ) ;
#6280=ORIENTED_EDGE ( 'NONE', *, *, #23306, .F. ) ;
#6281=CYLINDRICAL_SURFACE ( 'NONE', #17706, 0.4062499999999997780 ) ;
#6287=DIRECTION ( 'NONE',  ( 0.8090181274631199626, 0.5597738724868831506, 0.1792843582611305941 ) ) ;
#6306=ORIENTED_EDGE ( 'NONE', *, *, #20136, .F. ) ;
#6308=EDGE_CURVE ( 'NONE', #19422, #14487, #10086, .T. ) ;
#6320=VERTEX_POINT ( 'NONE', #3281 ) ;
#6361=EDGE_CURVE ( 'NONE', #12233, #16427, #6527, .T. ) ;
#6364=ORIENTED_EDGE ( 'NONE', *, *, #17324, .T. ) ;
#6376=ORIENTED_EDGE ( 'NONE', *, *, #12032, .F. ) ;
#6383=DIRECTION ( 'NONE',  ( -0.5773502691896258421, -0.5773502691896258421, -0.5773502691896258421 ) ) ;
#6390=DIRECTION ( 'NONE',  ( 0.000000000000000000, 0.000000000000000000, -1.000000000000000000 ) ) ;
#6412=CARTESIAN_POINT ( 'NONE',  ( 1.998815303304990465, 2.291712385858714729, -2.661240473580836152 ) ) ;
#6428=CARTESIAN_POINT ( 'NONE',  ( 0.3950000000000000178, 0.05000000000000028727, -2.591000000000000192 ) ) ;
#6432=ORIENTED_EDGE ( 'NONE', *, *, #19371, .T. ) ;
#6451=EDGE_LOOP ( 'NONE', ( #6432, #4024, #1251, #17987, #52, #6280, #15549 ) ) ;
#6457=DIRECTION ( 'NONE',  ( -0.8651979924482607887, 0.04370253788966922681, 0.4995222938423283798 ) ) ;
#6465=LINE ( 'NONE', #8290, #7540 ) ;
#6467=DIRECTION ( 'NONE',  ( -0.5850251379555668763, 0.7373335635563863510, 0.3377644208813451177 ) ) ;
#6473=DIRECTION ( 'NONE',  ( 0.000000000000000000, -0.9961946980917454342, 0.08715574274765829077 ) ) ;
#6496=ADVANCED_FACE ( 'NONE', ( #23334 ), #14093, .F. ) ;
#6507=ORIENTED_EDGE ( 'NONE', *, *, #14381, .F. ) ;
#6519=EDGE_LOOP ( 'NONE', ( #6306, #17738, #22618, #15420, #1416 ) ) ;
#6521=CARTESIAN_POINT ( 'NONE',  ( 2.094306190944884349, 2.923228049659837069, -2.986000000000000210 ) ) ;
#6527=LINE ( 'NONE', #4695, #6165 ) ;
#6538=AXIS2_PLACEMENT_3D ( 'NONE', #2440, #17310, #8272 ) ;
#6566=LINE ( 'NONE', #8638, #16661 ) ;
#6568=LINE ( 'NONE', #4501, #12601 ) ;
#6570=ORIENTED_EDGE ( 'NONE', *, *, #3752, .T. ) ;
#6579=CARTESIAN_POINT ( 'NONE',  ( 1.020000000000000018, 2.665000000000000036, -2.591000000000000192 ) ) ;
#6583=PLANE ( 'NONE',  #18307 ) ;
#6590=DIRECTION ( 'NONE',  ( -1.000000000000000000, 0.000000000000000000, 0.000000000000000000 ) ) ;
#6607=AXIS2_PLACEMENT_3D ( 'NONE', #17949, #878, #13937 ) ;
#6622=CARTESIAN_POINT ( 'NONE',  ( 2.168722887430706070, 2.291712385858714729, -1.763529041877836212 ) ) ;
#6626=LINE ( 'NONE', #15660, #4777 ) ;
#6634=ORIENTED_EDGE ( 'NONE', *, *, #2627, .T. ) ;
#6672=EDGE_CURVE ( 'NONE', #13943, #7960, #293, .T. ) ;
#6712=CARTESIAN_POINT ( 'NONE',  ( 0.8119709581221709049, 2.291712385858714285, -1.528283969076322801 ) ) ;
#6719=VECTOR ( 'NONE', #18266, 39.37007874015748143 ) ;
#6722=ADVANCED_FACE ( 'NONE', ( #15179 ), #22615, .F. ) ;
#6742=DIRECTION ( 'NONE',  ( 0.4985709748471344183, 0.07555085810113186529, 0.8635502596144365439 ) ) ;
#6746=CARTESIAN_POINT ( 'NONE',  ( 1.990730333795405205, 2.661358883302036293, -2.647236895612580021 ) ) ;
#6753=AXIS2_PLACEMENT_3D ( 'NONE', #14134, #8037, #13903 ) ;
#6757=EDGE_CURVE ( 'NONE', #19892, #14569, #22123, .T. ) ;
#6762=CARTESIAN_POINT ( 'NONE',  ( 0.3387631043874195225, 2.661358883302036293, -0.9952696662045950049 ) ) ;
#6780=ADVANCED_FACE ( 'NONE', ( #15535 ), #23074, .T. ) ;
#6782=ADVANCED_FACE ( 'NONE', ( #13720 ), #21140, .F. ) ;
#6787=ORIENTED_EDGE ( 'NONE', *, *, #4886, .T. ) ;
#6800=DIRECTION ( 'NONE',  ( -0.000000000000000000, -1.000000000000000000, -0.000000000000000000 ) ) ;
#6806=DIRECTION ( 'NONE',  ( 0.000000000000000000, -0.000000000000000000, -1.000000000000000000 ) ) ;
#6819=VECTOR ( 'NONE', #23393, 39.37007874015748854 ) ;
#6831=CARTESIAN_POINT ( 'NONE',  ( 0.7333413623369199330, 2.740000000000000213, -0.4233948329531084243 ) ) ;
#6833=CARTESIAN_POINT ( 'NONE',  ( 0.4700000000000000844, 2.740000000000000213, -0.05000000000000028727 ) ) ;
#6837=DIRECTION ( 'NONE',  ( -0.000000000000000000, -1.000000000000000000, -0.000000000000000000 ) ) ;
#6842=VECTOR ( 'NONE', #2160, 39.37007874015748143 ) ;
#6846=DIRECTION ( 'NONE',  ( -0.7071067811865436870, -0.7071067811865514585, -0.000000000000000000 ) ) ;
#6853=VERTEX_POINT ( 'NONE', #2379 ) ;
#6876=VECTOR ( 'NONE', #15619, 39.37007874015748143 ) ;
#6883=VERTEX_POINT ( 'NONE', #21857 ) ;
#6898=CARTESIAN_POINT ( 'NONE',  ( 0.4700000000000001954, 2.740000000000000213, 0.000000000000000000 ) ) ;
#6912=DIRECTION ( 'NONE',  ( 0.8660254037844383745, 0.000000000000000000, 0.5000000000000004441 ) ) ;
#6934=DIRECTION ( 'NONE',  ( 0.000000000000000000, -1.000000000000000000, 0.000000000000000000 ) ) ;
#6941=VECTOR ( 'NONE', #4090, 39.37007874015748143 ) ;
#6960=ORIENTED_EDGE ( 'NONE', *, *, #22035, .F. ) ;
#6962=DIRECTION ( 'NONE',  ( 0.3273051541876792481, 0.6681584153635196088, -0.6681584153635196088 ) ) ;
#6970=EDGE_LOOP ( 'NONE', ( #15027, #23786, #11270, #7447 ) ) ;
#6979=DIRECTION ( 'NONE',  ( -0.000000000000000000, -1.000000000000000000, 0.000000000000000000 ) ) ;
#6981=ORIENTED_EDGE ( 'NONE', *, *, #13947, .T. ) ;
#7014=ORIENTED_EDGE ( 'NONE', *, *, #3237, .T. ) ;
#7022=DIRECTION ( 'NONE',  ( -0.000000000000000000, -0.9961946980917454342, 0.08715574274765830465 ) ) ;
#7051=VERTEX_POINT ( 'NONE', #18499 ) ;
#7054=CARTESIAN_POINT ( 'NONE',  ( 1.573500000000000343, 0.5250000000000000222, -0.5399999999999998135 ) ) ;
#7067=EDGE_CURVE ( 'NONE', #4071, #10339, #1674, .T. ) ;
#7090=EDGE_CURVE ( 'NONE', #15406, #13943, #10952, .T. ) ;
#7093=EDGE_LOOP ( 'NONE', ( #6376, #19796, #19819, #15167, #17780, #15566 ) ) ;
#7104=DIRECTION ( 'NONE',  ( 0.000000000000000000, 0.000000000000000000, -1.000000000000000000 ) ) ;
#7116=CARTESIAN_POINT ( 'NONE',  ( 1.109470958122166229, 2.291712385858714285, -1.012998853824579104 ) ) ;
#7128=AXIS2_PLACEMENT_3D ( 'NONE', #20879, #3820, #11263 ) ;
#7130=ORIENTED_EDGE ( 'NONE', *, *, #7067, .F. ) ;
#7138=CARTESIAN_POINT ( 'NONE',  ( 0.7919466436700954848, 0.05000000000000028727, -2.986000000000000210 ) ) ;
#7140=PLANE ( 'NONE',  #1397 ) ;
#7147=VECTOR ( 'NONE', #14018, 39.37007874015748854 ) ;
#7156=EDGE_LOOP ( 'NONE', ( #21680, #10821, #13322, #12996 ) ) ;
#7181=LINE ( 'NONE', #5342, #37 ) ;
#7183=ORIENTED_EDGE ( 'NONE', *, *, #6672, .F. ) ;
#7196=ADVANCED_FACE ( 'NONE', ( #207 ), #2525, .F. ) ;
#7225=ORIENTED_EDGE ( 'NONE', *, *, #17461, .T. ) ;
#7263=VERTEX_POINT ( 'NONE', #690 ) ;
#7278=VECTOR ( 'NONE', #5389, 39.37007874015748143 ) ;
#7296=CARTESIAN_POINT ( 'NONE',  ( 2.936000000000000387, -3.638933710489514981E-33, -2.591000000000000636 ) ) ;
#7308=VECTOR ( 'NONE', #1421, 39.37007874015748143 ) ;
#7312=DIRECTION ( 'NONE',  ( -0.000000000000000000, -1.000000000000000000, -0.000000000000000000 ) ) ;
#7320=ORIENTED_EDGE ( 'NONE', *, *, #18698, .T. ) ;
#7328=CARTESIAN_POINT ( 'NONE',  ( 2.936000000000001720, 2.740000000000000213, 0.000000000000000000 ) ) ;
#7333=EDGE_CURVE ( 'NONE', #20229, #1954, #13983, .T. ) ;
#7341=EDGE_LOOP ( 'NONE', ( #10246, #4901, #19695, #11869, #10196 ) ) ;
#7342=ORIENTED_EDGE ( 'NONE', *, *, #14854, .T. ) ;
#7365=EDGE_LOOP ( 'NONE', ( #18810, #8995, #1558, #14276 ) ) ;
#7391=EDGE_CURVE ( 'NONE', #18827, #11232, #8234, .T. ) ;
#7400=ADVANCED_FACE ( 'NONE', ( #923 ), #3325, .T. ) ;
#7415=LINE ( 'NONE', #7296, #21315 ) ;
#7417=VECTOR ( 'NONE', #19637, 39.37007874015748854 ) ;
#7445=DIRECTION ( 'NONE',  ( 1.000000000000000000, 1.493785812010397745E-17, 1.707404996040164512E-16 ) ) ;
#7447=ORIENTED_EDGE ( 'NONE', *, *, #9157, .F. ) ;
#7458=ORIENTED_EDGE ( 'NONE', *, *, #7465, .F. ) ;
#7465=EDGE_CURVE ( 'NONE', #14874, #9859, #21669, .T. ) ;
#7468=DIRECTION ( 'NONE',  ( 0.000000000000000000, 0.000000000000000000, -1.000000000000000000 ) ) ;
#7508=AXIS2_PLACEMENT_3D ( 'NONE', #3875, #5701, #213 ) ;
#7513=CARTESIAN_POINT ( 'NONE',  ( 0.3950000000000000178, 2.665000000000000036, -1.966000000000000192 ) ) ;
#7534=CARTESIAN_POINT ( 'NONE',  ( 0.8119709581221709049, 2.978485840173427324, -1.588368860739399313 ) ) ;
#7537=DIRECTION ( 'NONE',  ( -0.8246458398455801531, 0.5656493956731305506, 0.000000000000000000 ) ) ;
#7540=VECTOR ( 'NONE', #22928, 39.37007874015747433 ) ;
#7550=CARTESIAN_POINT ( 'NONE',  ( 2.100416254512341485, 2.978485840173427324, -2.201288568297000925 ) ) ;
#7563=CARTESIAN_POINT ( 'NONE',  ( 1.573500000000000343, -3.414809992080329023E-17, -1.412500000000000089 ) ) ;
#7569=LINE ( 'NONE', #11237, #11894 ) ;
#7577=CARTESIAN_POINT ( 'NONE',  ( 2.936000000000001720, 2.740000000000000213, -0.05000000000000028727 ) ) ;
#7579=VERTEX_POINT ( 'NONE', #3629 ) ;
#7593=ADVANCED_FACE ( 'NONE', ( #11080 ), #14252, .F. ) ;
#7609=ORIENTED_EDGE ( 'NONE', *, *, #17461, .F. ) ;
#7614=VERTEX_POINT ( 'NONE', #18027 ) ;
#7622=DIRECTION ( 'NONE',  ( 0.000000000000000000, -1.000000000000000000, 0.000000000000000000 ) ) ;
#7629=ORIENTED_EDGE ( 'NONE', *, *, #16816, .F. ) ;
#7648=DIRECTION ( 'NONE',  ( -0.8660254037844434816, 0.000000000000000000, 0.4999999999999913403 ) ) ;
#7650=DIRECTION ( 'NONE',  ( -0.5000000000000043299, 0.000000000000000000, 0.8660254037844362651 ) ) ;
#7659=ORIENTED_EDGE ( 'NONE', *, *, #23418, .T. ) ;
#7686=EDGE_CURVE ( 'NONE', #20226, #397, #19323, .T. ) ;
#7688=EDGE_CURVE ( 'NONE', #22655, #17146, #3993, .T. ) ;
#7695=ADVANCED_FACE ( 'NONE', ( #15662 ), #5820, .T. ) ;
#7701=CARTESIAN_POINT ( 'NONE',  ( 2.100109879709019189, 2.740000000000000213, -3.013126998327187778 ) ) ;
#7706=CARTESIAN_POINT ( 'NONE',  ( 0.7847114317029997288, 0.000000000000000000, -0.6249999999999962252 ) ) ;
#7721=ADVANCED_FACE ( 'NONE', ( #2177 ), #16327, .F. ) ;
#7733=DIRECTION ( 'NONE',  ( 0.000000000000000000, -0.7071067811865464625, -0.7071067811865486830 ) ) ;
#7734=ORIENTED_EDGE ( 'NONE', *, *, #2767, .T. ) ;
#7781=ORIENTED_EDGE ( 'NONE', *, *, #9928, .T. ) ;
#7802=FACE_OUTER_BOUND ( 'NONE', #12045, .T. ) ;
#7817=CARTESIAN_POINT ( 'NONE',  ( 0.8977114317029943891, 2.291712385858714729, -0.6297771125693037986 ) ) ;
#7836=EDGE_CURVE ( 'NONE', #10167, #19328, #11201, .T. ) ;
#7847=CARTESIAN_POINT ( 'NONE',  ( 1.964169762594504265, 2.687712728237018567, -2.661240473580835708 ) ) ;
#7857=CARTESIAN_POINT ( 'NONE',  ( 3.194613732291736063, 1.301349684034776022, -3.842349684034790602 ) ) ;
#7862=ORIENTED_EDGE ( 'NONE', *, *, #11812, .F. ) ;
#7885=CARTESIAN_POINT ( 'NONE',  ( 1.766928915791902144, 2.471730513698206178, -1.986411895277231832 ) ) ;
#7888=EDGE_CURVE ( 'NONE', #19306, #8464, #91, .T. ) ;
#7894=VECTOR ( 'NONE', #22013, 39.37007874015747433 ) ;
#7911=VECTOR ( 'NONE', #19039, 39.37007874015748143 ) ;
#7914=CARTESIAN_POINT ( 'NONE',  ( 0.4172595264191667486, 2.291712385858714285, -0.8269699969948853813 ) ) ;
#7916=EDGE_LOOP ( 'NONE', ( #22829, #1160, #10521, #14711, #15082, #18235, #9202, #14626, #12826, #13265 ) ) ;
#7929=LINE ( 'NONE', #11856, #7911 ) ;
#7936=EDGE_CURVE ( 'NONE', #18537, #1154, #17730, .T. ) ;
#7944=CARTESIAN_POINT ( 'NONE',  ( 2.336126731229780429, 2.690142902515283208, -2.565857097484717020 ) ) ;
#7960=VERTEX_POINT ( 'NONE', #10306 ) ;
#7966=AXIS2_PLACEMENT_3D ( 'NONE', #23145, #6457, #21455 ) ;
#7975=DIRECTION ( 'NONE',  ( -0.3273051541876813575, -0.6681584153635157231, 0.6681584153635227175 ) ) ;
#7983=VECTOR ( 'NONE', #3743, 39.37007874015748143 ) ;
#7999=ORIENTED_EDGE ( 'NONE', *, *, #20136, .T. ) ;
#8014=AXIS2_PLACEMENT_3D ( 'NONE', #13202, #20615, #3915 ) ;
#8017=EDGE_CURVE ( 'NONE', #7263, #19306, #21869, .T. ) ;
#8018=FACE_OUTER_BOUND ( 'NONE', #14095, .T. ) ;
#8019=ADVANCED_FACE ( 'NONE', ( #23320 ), #16024, .F. ) ;
#8020=ORIENTED_EDGE ( 'NONE', *, *, #17324, .F. ) ;
#8027=EDGE_LOOP ( 'NONE', ( #20533, #1648, #3415 ) ) ;
#8037=DIRECTION ( 'NONE',  ( 0.000000000000000000, 1.000000000000000000, 0.000000000000000000 ) ) ;
#8038=ORIENTED_EDGE ( 'NONE', *, *, #14595, .F. ) ;
#8054=VERTEX_POINT ( 'NONE', #17857 ) ;
#8056=CARTESIAN_POINT ( 'NONE',  ( 0.4700000000000001954, 2.740000000000000213, -1.836096189432333103 ) ) ;
#8060=DIRECTION ( 'NONE',  ( -0.5773502691896257311, -0.5773502691896257311, -0.5773502691896257311 ) ) ;
#8072=VERTEX_POINT ( 'NONE', #2847 ) ;
#8079=ORIENTED_EDGE ( 'NONE', *, *, #18910, .T. ) ;
#8095=ORIENTED_EDGE ( 'NONE', *, *, #15927, .T. ) ;
#8108=VECTOR ( 'NONE', #22325, 39.37007874015748854 ) ;
#8132=AXIS2_PLACEMENT_3D ( 'NONE', #21172, #10783, #1504 ) ;
#8142=FACE_OUTER_BOUND ( 'NONE', #11125, .T. ) ;
#8144=VERTEX_POINT ( 'NONE', #23058 ) ;
#8152=DIRECTION ( 'NONE',  ( 0.7071067811865475727, 0.000000000000000000, 0.7071067811865474617 ) ) ;
#8163=VECTOR ( 'NONE', #16933, 39.37007874015748143 ) ;
#8165=VECTOR ( 'NONE', #1183, 39.37007874015748143 ) ;
#8168=CARTESIAN_POINT ( 'NONE',  ( 1.573500000000000121, 0.6376613660676677675, -0.3524999999999999800 ) ) ;
#8186=ORIENTED_EDGE ( 'NONE', *, *, #18271, .F. ) ;
#8234=LINE ( 'NONE', #11926, #22168 ) ;
#8249=DIRECTION ( 'NONE',  ( 0.5773502691896257311, -0.5773502691896257311, 0.5773502691896257311 ) ) ;
#8250=VERTEX_POINT ( 'NONE', #22830 ) ;
#8255=EDGE_CURVE ( 'NONE', #6883, #6320, #17345, .T. ) ;
#8256=VECTOR ( 'NONE', #9301, 39.37007874015748854 ) ;
#8261=LINE ( 'NONE', #4721, #3012 ) ;
#8272=DIRECTION ( 'NONE',  ( 0.5000000000000007772, 0.000000000000000000, 0.8660254037844382635 ) ) ;
#8279=VECTOR ( 'NONE', #15400, 39.37007874015748854 ) ;
#8282=CARTESIAN_POINT ( 'NONE',  ( 0.4450000000000002842, 0.000000000000000000, -1.879397459621555244 ) ) ;
#8284=EDGE_CURVE ( 'NONE', #11232, #14303, #18942, .T. ) ;
#8290=CARTESIAN_POINT ( 'NONE',  ( 0.5550849365154918447, 2.740000000000000213, -0.7321440192514540035 ) ) ;
#8292=DIRECTION ( 'NONE',  ( -0.5773502691896256200, 0.5773502691896194028, -0.5773502691896320593 ) ) ;
#8299=LINE ( 'NONE', #19520, #21036 ) ;
#8305=LINE ( 'NONE', #3728, #17438 ) ;
#8308=ORIENTED_EDGE ( 'NONE', *, *, #16480, .F. ) ;
#8313=ORIENTED_EDGE ( 'NONE', *, *, #17163, .T. ) ;
#8315=VERTEX_POINT ( 'NONE', #4653 ) ;
#8316=CARTESIAN_POINT ( 'NONE',  ( 3.025220084236446727, 2.291712385858714729, -2.986000000000001098 ) ) ;
#8321=ADVANCED_FACE ( 'NONE', ( #14289 ), #8667, .T. ) ;
#8323=DIRECTION ( 'NONE',  ( 0.000000000000000000, 0.000000000000000000, 1.000000000000000000 ) ) ;
#8333=CARTESIAN_POINT ( 'NONE',  ( 1.573500000000000343, 0.000000000000000000, -0.3524999999999999800 ) ) ;
#8362=ORIENTED_EDGE ( 'NONE', *, *, #21874, .T. ) ;
#8365=EDGE_CURVE ( 'NONE', #16517, #24032, #23653, .T. ) ;
#8386=DIRECTION ( 'NONE',  ( 1.000000000000000000, 0.000000000000000000, -0.000000000000000000 ) ) ;
#8391=CARTESIAN_POINT ( 'NONE',  ( 2.310583317527613811, 2.687712728237018567, -2.461238514389269660 ) ) ;
#8413=PLANE ( 'NONE',  #23569 ) ;
#8427=ADVANCED_FACE ( 'NONE', ( #3071 ), #2825, .T. ) ;
#8439=LINE ( 'NONE', #3312, #5408 ) ;
#8451=FACE_OUTER_BOUND ( 'NONE', #15091, .T. ) ;
#8453=CARTESIAN_POINT ( 'NONE',  ( 2.356222887430696744, 2.291712385858714729, -2.088288568297006265 ) ) ;
#8464=VERTEX_POINT ( 'NONE', #5127 ) ;
#8487=DIRECTION ( 'NONE',  ( 0.4995222938423188319, 0.04370253788966847047, -0.8651979924482662287 ) ) ;
#8502=CARTESIAN_POINT ( 'NONE',  ( 2.725416254512337932, 0.04999999999999973910, -2.591000000000000636 ) ) ;
#8506=DIRECTION ( 'NONE',  ( -0.5773502691896278405, 0.5773502691896214012, 0.5773502691896278405 ) ) ;
#8513=PLANE ( 'NONE',  #22101 ) ;
#8554=DIRECTION ( 'NONE',  ( -0.4999999999999911737, 2.705315378517703502E-18, 0.8660254037844437036 ) ) ;
#8577=VECTOR ( 'NONE', #18247, 39.37007874015748854 ) ;
#8580=CARTESIAN_POINT ( 'NONE',  ( 1.644486777265590005, 2.661358883302036293, -2.047525463909579457 ) ) ;
#8581=ORIENTED_EDGE ( 'NONE', *, *, #1721, .F. ) ;
#8587=CARTESIAN_POINT ( 'NONE',  ( 0.8119709581221709049, 2.291712385858714729, -1.528283969076322801 ) ) ;
#8596=VECTOR ( 'NONE', #5955, 39.37007874015748854 ) ;
#8597=ORIENTED_EDGE ( 'NONE', *, *, #10667, .F. ) ;
#8600=CARTESIAN_POINT ( 'NONE',  ( 1.457716030923678074, 2.291712385858714729, -2.174029041877829194 ) ) ;
#8605=ORIENTED_EDGE ( 'NONE', *, *, #9881, .F. ) ;
#8618=ORIENTED_EDGE ( 'NONE', *, *, #20351, .F. ) ;
#8627=LINE ( 'NONE', #9995, #674 ) ;
#8638=CARTESIAN_POINT ( 'NONE',  ( 0.000000000000000000, 0.05000000000000028727, -0.5991858428704237571 ) ) ;
#8667=PLANE ( 'NONE',  #6607 ) ;
#8703=EDGE_CURVE ( 'NONE', #5136, #3473, #23030, .T. ) ;
#8725=EDGE_CURVE ( 'NONE', #24096, #22560, #23382, .T. ) ;
#8731=EDGE_CURVE ( 'NONE', #19257, #23449, #19498, .T. ) ;
#8745=CARTESIAN_POINT ( 'NONE',  ( 1.573500000000000343, -3.414809992080329023E-17, -0.3524999999999999800 ) ) ;
#8751=PLANE ( 'NONE',  #9254 ) ;
#8760=AXIS2_PLACEMENT_3D ( 'NONE', #12065, #14967, #16793 ) ;
#8772=LINE ( 'NONE', #12341, #12513 ) ;
#8777=ORIENTED_EDGE ( 'NONE', *, *, #5573, .T. ) ;
#8781=CARTESIAN_POINT ( 'NONE',  ( 1.573500000000000343, 0.05625000000000004996, -1.818749999999999867 ) ) ;
#8804=EDGE_LOOP ( 'NONE', ( #4667, #2394, #8906, #10199, #2248 ) ) ;
#8813=LINE ( 'NONE', #4674, #19364 ) ;
#8820=ORIENTED_EDGE ( 'NONE', *, *, #21838, .T. ) ;
#8821=AXIS2_PLACEMENT_3D ( 'NONE', #16575, #14630, #4982 ) ;
#8862=CARTESIAN_POINT ( 'NONE',  ( 0.8208141571295791694, 2.690000000000002167, -2.986000000000000210 ) ) ;
#8906=ORIENTED_EDGE ( 'NONE', *, *, #19643, .T. ) ;
#8923=AXIS2_PLACEMENT_3D ( 'NONE', #5706, #9611, #6390 ) ;
#8932=PLANE ( 'NONE',  #17168 ) ;
#8979=ORIENTED_EDGE ( 'NONE', *, *, #12124, .F. ) ;
#8995=ORIENTED_EDGE ( 'NONE', *, *, #16334, .T. ) ;
#9041=LINE ( 'NONE', #1485, #13494 ) ;
#9045=DIRECTION ( 'NONE',  ( -0.7071067811865475727, -0.7071067811865475727, -0.000000000000000000 ) ) ;
#9046=CARTESIAN_POINT ( 'NONE',  ( 2.369221741255291391, 0.000000000000000000, -1.763529041877836434 ) ) ;
#9048=VERTEX_POINT ( 'NONE', #6183 ) ;
#9061=DIRECTION ( 'NONE',  ( 0.8635502596144278842, 0.07555085810113110201, 0.4985709748471494618 ) ) ;
#9063=DIRECTION ( 'NONE',  ( 0.000000000000000000, 0.000000000000000000, -1.000000000000000000 ) ) ;
#9080=CARTESIAN_POINT ( 'NONE',  ( 1.573500000000000343, -3.414809992080329023E-17, -1.875000000000000000 ) ) ;
#9085=CONICAL_SURFACE ( 'NONE', #6753, 0.4062499999999995004, 0.7853981633974482790 ) ;
#9108=ORIENTED_EDGE ( 'NONE', *, *, #17048, .T. ) ;
#9113=CARTESIAN_POINT ( 'NONE',  ( 1.967764614661186462, 2.340112590966282546, -1.877107582790499052 ) ) ;
#9117=VECTOR ( 'NONE', #9851, 39.37007874015748143 ) ;
#9123=ORIENTED_EDGE ( 'NONE', *, *, #22229, .F. ) ;
#9125=ADVANCED_FACE ( 'NONE', ( #18634 ), #17045, .T. ) ;
#9127=AXIS2_PLACEMENT_3D ( 'NONE', #15878, #23181, #23294 ) ;
#9132=CARTESIAN_POINT ( 'NONE',  ( 1.573500000000000343, 0.05625000000000004996, -1.412500000000000089 ) ) ;
#9145=MANIFOLD_SOLID_BREP ( 'Chamfer2 .050"', #20082 ) ;
#9147=VERTEX_POINT ( 'NONE', #4297 ) ;
#9157=EDGE_CURVE ( 'NONE', #20226, #19257, #9372, .T. ) ;
#9164=FACE_OUTER_BOUND ( 'NONE', #22141, .T. ) ;
#9168=ORIENTED_EDGE ( 'NONE', *, *, #1131, .F. ) ;
#9177=CARTESIAN_POINT ( 'NONE',  ( 0.9396693423734434614, 2.384778440500604280, -1.315246104248910530 ) ) ;
#9194=VECTOR ( 'NONE', #11724, 39.37007874015748854 ) ;
#9202=ORIENTED_EDGE ( 'NONE', *, *, #2472, .F. ) ;
#9208=ORIENTED_EDGE ( 'NONE', *, *, #19371, .F. ) ;
#9220=EDGE_CURVE ( 'NONE', #9147, #14303, #931, .T. ) ;
#9225=PLANE ( 'NONE',  #17387 ) ;
#9228=VECTOR ( 'NONE', #261, 39.37007874015748854 ) ;
#9231=LINE ( 'NONE', #18616, #7983 ) ;
#9244=VECTOR ( 'NONE', #19189, 39.37007874015748143 ) ;
#9249=EDGE_LOOP ( 'NONE', ( #14452, #13759, #17510, #23704, #21354 ) ) ;
#9254=AXIS2_PLACEMENT_3D ( 'NONE', #10242, #6934, #10126 ) ;
#9257=CARTESIAN_POINT ( 'NONE',  ( 1.573500000000000343, 2.740000000000000213, -1.874999999999999334 ) ) ;
#9263=DIRECTION ( 'NONE',  ( -0.000000000000000000, -1.000000000000000000, -0.000000000000000000 ) ) ;
#9266=ORIENTED_EDGE ( 'NONE', *, *, #13222, .F. ) ;
#9275=ORIENTED_EDGE ( 'NONE', *, *, #21097, .T. ) ;
#9276=VECTOR ( 'NONE', #5047, 39.37007874015748143 ) ;
#9286=AXIS2_PLACEMENT_3D ( 'NONE', #22958, #6383, #6260 ) ;
#9287=ORIENTED_EDGE ( 'NONE', *, *, #23604, .T. ) ;
#9291=CARTESIAN_POINT ( 'NONE',  ( 0.7919466436700954848, 0.05000000000000028727, -2.986000000000000210 ) ) ;
#9298=CARTESIAN_POINT ( 'NONE',  ( 0.9765096322779955873, 2.453214835500605595, -1.257424259103740116 ) ) ;
#9301=DIRECTION ( 'NONE',  ( 0.5773502691896256200, 0.5773502691896257311, -0.5773502691896257311 ) ) ;
#9310=VECTOR ( 'NONE', #18379, 39.37007874015748143 ) ;
#9322=ORIENTED_EDGE ( 'NONE', *, *, #11219, .F. ) ;
#9331=ORIENTED_EDGE ( 'NONE', *, *, #7090, .F. ) ;
#9354=DIRECTION ( 'NONE',  ( 0.8660254037844433705, 0.000000000000000000, 0.4999999999999916178 ) ) ;
#9369=DIRECTION ( 'NONE',  ( -0.7071067811865475727, -0.7071067811865475727, -0.000000000000000000 ) ) ;
#9371=PLANE ( 'NONE',  #11331 ) ;
#9372=LINE ( 'NONE', #15342, #17502 ) ;
#9379=ADVANCED_FACE ( 'NONE', ( #4474 ), #2879, .T. ) ;
#9380=CARTESIAN_POINT ( 'NONE',  ( 1.471352214327352081, 2.291712385858714285, -1.221931094509318694 ) ) ;
#9396=DIRECTION ( 'NONE',  ( -0.8660254037844434816, 0.000000000000000000, 0.4999999999999913403 ) ) ;
#9421=CARTESIAN_POINT ( 'NONE',  ( 1.101325272654156251, 2.384774948516263482, -1.035249514148854466 ) ) ;
#9426=DIRECTION ( 'NONE',  ( -0.000000000000000000, -1.000000000000000000, -0.000000000000000000 ) ) ;
#9432=EDGE_CURVE ( 'NONE', #20425, #22988, #12296, .T. ) ;
#9433=( CONVERSION_BASED_UNIT ( 'INCH', #1995 ) LENGTH_UNIT ( ) NAMED_UNIT ( #17887 ) );
#9458=EDGE_CURVE ( 'NONE', #363, #23278, #4826, .T. ) ;
#9482=EDGE_CURVE ( 'NONE', #21880, #5470, #5318, .T. ) ;
#9483=CARTESIAN_POINT ( 'NONE',  ( 0.8977114317029943891, 0.000000000000000000, -0.4292782587447178111 ) ) ;
#9489=DIRECTION ( 'NONE',  ( 8.659560562354947649E-17, -0.7071067811865464625, 0.7071067811865486830 ) ) ;
#9508=CARTESIAN_POINT ( 'NONE',  ( 0.3950000000000000178, 0.000000000000000000, -0.04999999999999918399 ) ) ;
#9533=CARTESIAN_POINT ( 'NONE',  ( 0.4200000000000000400, 2.689999999999999947, -2.566000000000000281 ) ) ;
#9554=ORIENTED_EDGE ( 'NONE', *, *, #21779, .T. ) ;
#9560=ORIENTED_EDGE ( 'NONE', *, *, #22713, .T. ) ;
#9576=CARTESIAN_POINT ( 'NONE',  ( 2.948500000000000121, 0.01249999999999952538, -0.03749999999999966555 ) ) ;
#9581=VERTEX_POINT ( 'NONE', #22140 ) ;
#9594=LINE ( 'NONE', #17872, #17354 ) ;
#9608=CARTESIAN_POINT ( 'NONE',  ( 1.652571746775178152, 2.291712385858714285, -2.061529041877830704 ) ) ;
#9611=DIRECTION ( 'NONE',  ( -0.000000000000000000, -1.000000000000000000, -0.000000000000000000 ) ) ;
#9614=VECTOR ( 'NONE', #21311, 39.37007874015748143 ) ;
#9627=CARTESIAN_POINT ( 'NONE',  ( 2.262531734667336369, 2.800838881557672355, -2.455161118442326984 ) ) ;
#9633=DIRECTION ( 'NONE',  ( 0.000000000000000000, 0.000000000000000000, -1.000000000000000000 ) ) ;
#9637=FACE_OUTER_BOUND ( 'NONE', #11577, .T. ) ;
#9661=DIRECTION ( 'NONE',  ( 1.000000000000000000, 0.000000000000000000, 0.000000000000000000 ) ) ;
#9671=CARTESIAN_POINT ( 'NONE',  ( 0.000000000000000000, 2.689999999999999947, 0.000000000000000000 ) ) ;
#9676=ORIENTED_EDGE ( 'NONE', *, *, #18875, .T. ) ;
#9680=LINE ( 'NONE', #17119, #968 ) ;
#9714=AXIS2_PLACEMENT_3D ( 'NONE', #4970, #12437, #3150 ) ;
#9728=CARTESIAN_POINT ( 'NONE',  ( 1.670753895751090790, 2.384778440500605168, -2.046330657626557858 ) ) ;
#9733=VECTOR ( 'NONE', #16087, 39.37007874015748854 ) ;
#9737=ADVANCED_FACE ( 'NONE', ( #22261 ), #15079, .F. ) ;
#9749=LINE ( 'NONE', #9627, #17537 ) ;
#9752=DIRECTION ( 'NONE',  ( -0.6546536707079757544, -0.6546536707079760875, -0.3779644730092315830 ) ) ;
#9788=CARTESIAN_POINT ( 'NONE',  ( -0.3882564258214251662, 2.740000000000000213, -0.6724798558878207766 ) ) ;
#9816=EDGE_LOOP ( 'NONE', ( #4178, #4446 ) ) ;
#9817=CARTESIAN_POINT ( 'NONE',  ( 2.936000000000000387, 0.000000000000000000, -0.07500000000000014988 ) ) ;
#9818=CARTESIAN_POINT ( 'NONE',  ( 1.887609879709022165, 2.740000000000000213, -2.645066201718798471 ) ) ;
#9828=ORIENTED_EDGE ( 'NONE', *, *, #19552, .T. ) ;
#9835=CARTESIAN_POINT ( 'NONE',  ( 0.3950000000000000178, 2.740039370078740433, -2.540999999999999925 ) ) ;
#9851=DIRECTION ( 'NONE',  ( -0.000000000000000000, -0.9961946980917454342, 0.08715574274765830465 ) ) ;
#9859=VERTEX_POINT ( 'NONE', #22217 ) ;
#9861=ORIENTED_EDGE ( 'NONE', *, *, #15927, .F. ) ;
#9863=VECTOR ( 'NONE', #21025, 39.37007874015748143 ) ;
#9866=DIRECTION ( 'NONE',  ( -1.493785812010397745E-17, 1.000000000000000000, 0.000000000000000000 ) ) ;
#9867=ORIENTED_EDGE ( 'NONE', *, *, #21809, .T. ) ;
#9881=EDGE_CURVE ( 'NONE', #14569, #11335, #2349, .T. ) ;
#9883=CARTESIAN_POINT ( 'NONE',  ( 0.4449999999999992295, 0.000000000000000000, -0.04999999999999918399 ) ) ;
#9885=PLANE ( 'NONE',  #22323 ) ;
#9910=EDGE_CURVE ( 'NONE', #24096, #16027, #20752, .T. ) ;
#9923=DIRECTION ( 'NONE',  ( -0.08715574274765833240, 0.9961946980917454342, 3.870492493070290181E-17 ) ) ;
#9928=EDGE_CURVE ( 'NONE', #19328, #19011, #5989, .T. ) ;
#9937=CARTESIAN_POINT ( 'NONE',  ( 0.3950000000000000733, 0.04999999999999864969, -0.4043744331762961775 ) ) ;
#9939=ADVANCED_FACE ( 'NONE', ( #4043 ), #13330, .F. ) ;
#9954=ORIENTED_EDGE ( 'NONE', *, *, #6032, .T. ) ;
#9966=ORIENTED_EDGE ( 'NONE', *, *, #20471, .F. ) ;
#9968=CARTESIAN_POINT ( 'NONE',  ( 0.6107956263425956545, 2.685901063997346405, -1.186814756611144883 ) ) ;
#9974=DIRECTION ( 'NONE',  ( 8.659560562354915602E-17, -0.7071067811865489050, 0.7071067811865461294 ) ) ;
#9980=PRODUCT_DEFINITION_FORMATION_WITH_SPECIFIED_SOURCE ( 'ANY', '', #19837, .NOT_KNOWN. ) ;
#9983=EDGE_LOOP ( 'NONE', ( #9123, #122, #10090, #17303 ) ) ;
#9995=CARTESIAN_POINT ( 'NONE',  ( 2.108637995767629114, 2.978485840173427324, -1.763529041877836434 ) ) ;
#10005=VECTOR ( 'NONE', #23390, 39.37007874015748854 ) ;
#10014=ADVANCED_FACE ( 'NONE', ( #22819 ), #6109, .F. ) ;
#10019=DIRECTION ( 'NONE',  ( -0.08715574274765833240, 0.9961946980917454342, 3.870492493070290181E-17 ) ) ;
#10040=ORIENTED_EDGE ( 'NONE', *, *, #15732, .T. ) ;
#10041=VECTOR ( 'NONE', #1502, 39.37007874015748143 ) ;
#10044=FACE_OUTER_BOUND ( 'NONE', #20387, .T. ) ;
#10048=EDGE_CURVE ( 'NONE', #4938, #12247, #16971, .T. ) ;
#10060=LINE ( 'NONE', #15658, #4300 ) ;
#10064=CARTESIAN_POINT ( 'NONE',  ( 0.3950000000000000178, 0.05000000000000028727, -2.591000000000000192 ) ) ;
#10068=EDGE_CURVE ( 'NONE', #19497, #21850, #20093, .T. ) ;
#10070=EDGE_CURVE ( 'NONE', #14874, #21142, #8299, .T. ) ;
#10086=CIRCLE ( 'NONE', #728, 0.1874999999999998335 ) ;
#10090=ORIENTED_EDGE ( 'NONE', *, *, #20361, .F. ) ;
#10116=CARTESIAN_POINT ( 'NONE',  ( 2.911000000000000032, 2.689999999999999947, 0.000000000000000000 ) ) ;
#10126=DIRECTION ( 'NONE',  ( 0.000000000000000000, -0.000000000000000000, -1.000000000000000000 ) ) ;
#10129=EDGE_LOOP ( 'NONE', ( #4502, #5260, #13893, #10245, #21512, #13249 ) ) ;
#10130=VERTEX_POINT ( 'NONE', #4527 ) ;
#10131=DIRECTION ( 'NONE',  ( 0.4472135954999560403, -0.4472135954999560403, 0.7745966692414856247 ) ) ;
#10135=ADVANCED_FACE ( 'NONE', ( #15751 ), #748, .F. ) ;
#10138=VECTOR ( 'NONE', #15062, 39.37007874015748143 ) ;
#10140=VECTOR ( 'NONE', #17099, 39.37007874015748854 ) ;
#10143=LINE ( 'NONE', #17567, #4673 ) ;
#10159=VECTOR ( 'NONE', #8506, 39.37007874015748854 ) ;
#10162=VERTEX_POINT ( 'NONE', #12676 ) ;
#10166=CARTESIAN_POINT ( 'NONE',  ( 1.397631139260601341, 2.978485840173427324, -2.174029041877829638 ) ) ;
#10167=VERTEX_POINT ( 'NONE', #19280 ) ;
#10172=FACE_OUTER_BOUND ( 'NONE', #23891, .T. ) ;
#10176=ORIENTED_EDGE ( 'NONE', *, *, #17163, .F. ) ;
#10183=DIRECTION ( 'NONE',  ( 0.08715574274765830465, -0.9961946980917454342, -3.870492493070289564E-17 ) ) ;
#10187=DIRECTION ( 'NONE',  ( 0.000000000000000000, 0.000000000000000000, -1.000000000000000000 ) ) ;
#10196=ORIENTED_EDGE ( 'NONE', *, *, #17114, .F. ) ;
#10197=FACE_OUTER_BOUND ( 'NONE', #17543, .T. ) ;
#10199=ORIENTED_EDGE ( 'NONE', *, *, #10667, .T. ) ;
#10205=DIRECTION ( 'NONE',  ( -0.08715574274765827689, 0.9961946980917454342, -5.815890212748468633E-18 ) ) ;
#10217=EDGE_CURVE ( 'NONE', #1943, #18699, #13482, .T. ) ;
#10228=CARTESIAN_POINT ( 'NONE',  ( 1.573500000000000343, 0.000000000000000000, -0.5399999999999998135 ) ) ;
#10230=DIRECTION ( 'NONE',  ( 0.000000000000000000, 0.000000000000000000, -1.000000000000000000 ) ) ;
#10236=DIRECTION ( 'NONE',  ( 0.000000000000000000, -1.000000000000000000, 0.000000000000000000 ) ) ;
#10242=CARTESIAN_POINT ( 'NONE',  ( 0.000000000000000000, 2.291712385858714729, 0.03922008423644621905 ) ) ;
#10243=DIRECTION ( 'NONE',  ( 0.08715574274765830465, -0.9961946980917454342, -3.870492493070289564E-17 ) ) ;
#10245=ORIENTED_EDGE ( 'NONE', *, *, #3372, .T. ) ;
#10246=ORIENTED_EDGE ( 'NONE', *, *, #17834, .T. ) ;
#10267=AXIS2_PLACEMENT_3D ( 'NONE', #1381, #6742, #12739 ) ;
#10270=CARTESIAN_POINT ( 'NONE',  ( 2.986000000000000210, 2.690000000000002167, 0.000000000000000000 ) ) ;
#10282=DIRECTION ( 'NONE',  ( 0.7071067811865514585, -0.7071067811865436870, 0.000000000000000000 ) ) ;
#10306=CARTESIAN_POINT ( 'NONE',  ( 1.573500000000000343, -3.414809992080329023E-17, -1.875000000000000000 ) ) ;
#10309=ORIENTED_EDGE ( 'NONE', *, *, #3946, .T. ) ;
#10316=ORIENTED_EDGE ( 'NONE', *, *, #4658, .F. ) ;
#10332=FACE_OUTER_BOUND ( 'NONE', #2325, .T. ) ;
#10339=VERTEX_POINT ( 'NONE', #20658 ) ;
#10348=ADVANCED_FACE ( 'NONE', ( #5781 ), #23193, .F. ) ;
#10356=ORIENTED_EDGE ( 'NONE', *, *, #16892, .F. ) ;
#10360=CARTESIAN_POINT ( 'NONE',  ( 0.000000000000000000, 0.000000000000000000, 0.000000000000000000 ) ) ;
#10367=ORIENTED_EDGE ( 'NONE', *, *, #4311, .F. ) ;
#10383=EDGE_CURVE ( 'NONE', #22560, #19497, #11893, .T. ) ;
#10384=DIRECTION ( 'NONE',  ( 0.6989184867586851757, -0.09025067990440575894, 0.7094841532012832186 ) ) ;
#10406=DIRECTION ( 'NONE',  ( 0.000000000000000000, 0.000000000000000000, 1.000000000000000000 ) ) ;
#10412=MECHANICAL_CONTEXT ( 'NONE', #18859, 'mechanical' ) ;
#10424=LINE ( 'NONE', #19917, #12379 ) ;
#10436=ORIENTED_EDGE ( 'NONE', *, *, #10048, .F. ) ;
#10438=ORIENTED_EDGE ( 'NONE', *, *, #2081, .F. ) ;
#10441=LINE ( 'NONE', #11912, #23533 ) ;
#10454=CARTESIAN_POINT ( 'NONE',  ( 0.3950000000000000178, 2.740039370078740433, -2.540999999999999925 ) ) ;
#10456=CARTESIAN_POINT ( 'NONE',  ( 0.3228671510180489701, 2.690047770615767941, -1.025312217484214639 ) ) ;
#10461=DIRECTION ( 'NONE',  ( -1.707404996040164512E-16, 0.000000000000000000, 1.000000000000000000 ) ) ;
#10471=CARTESIAN_POINT ( 'NONE',  ( 0.1430000000000000993, 2.833000000000000185, -1.917502577388072282 ) ) ;
#10482=CARTESIAN_POINT ( 'NONE',  ( 0.4872114317030045716, 2.291712385858715173, -1.340783969076326132 ) ) ;
#10487=ADVANCED_FACE ( 'NONE', ( #18438 ), #23548, .T. ) ;
#10509=EDGE_CURVE ( 'NONE', #6154, #19422, #24035, .T. ) ;
#10518=ADVANCED_FACE ( 'NONE', ( #14429 ), #8932, .F. ) ;
#10521=ORIENTED_EDGE ( 'NONE', *, *, #10998, .T. ) ;
#10529=ORIENTED_EDGE ( 'NONE', *, *, #199, .F. ) ;
#10532=CARTESIAN_POINT ( 'NONE',  ( 0.05000000000000028727, 2.740000000000000213, 0.000000000000000000 ) ) ;
#10542=FACE_OUTER_BOUND ( 'NONE', #348, .T. ) ;
#10545=DIRECTION ( 'NONE',  ( -0.7745966692414841814, -0.4472135954999572061, -0.4472135954999572061 ) ) ;
#10553=VECTOR ( 'NONE', #9923, 39.37007874015748143 ) ;
#10577=AXIS2_PLACEMENT_3D ( 'NONE', #7914, #15365, #6088 ) ;
#10586=CARTESIAN_POINT ( 'NONE',  ( 0.03174294256098301320, 2.685901063997346405, -0.8524985337548631747 ) ) ;
#10600=CARTESIAN_POINT ( 'NONE',  ( 1.020000000000000018, 2.740039370078740433, -2.591000000000000192 ) ) ;
#10601=LINE ( 'NONE', #12685, #14064 ) ;
#10638=VECTOR ( 'NONE', #13227, 39.37007874015748854 ) ;
#10643=EDGE_LOOP ( 'NONE', ( #8313, #22144, #5235, #3635 ) ) ;
#10646=DIRECTION ( 'NONE',  ( 0.3535533905932763954, -0.7071067811865482389, -0.6123724356957921389 ) ) ;
#10667=EDGE_CURVE ( 'NONE', #5661, #12271, #20626, .T. ) ;
#10675=PLANE ( 'NONE',  #826 ) ;
#10685=VERTEX_POINT ( 'NONE', #4521 ) ;
#10694=AXIS2_PLACEMENT_3D ( 'NONE', #10166, #880, #2827 ) ;
#10708=AXIS2_PLACEMENT_3D ( 'NONE', #5715, #12937, #18515 ) ;
#10740=DIRECTION ( 'NONE',  ( 1.493785812010397745E-17, -1.000000000000000000, 0.000000000000000000 ) ) ;
#10752=PLANE ( 'NONE',  #20174 ) ;
#10753=DIRECTION ( 'NONE',  ( -0.000000000000000000, -0.6546536707079746442, -0.7559289460184566156 ) ) ;
#10763=VECTOR ( 'NONE', #11479, 39.37007874015748143 ) ;
#10766=ORIENTED_EDGE ( 'NONE', *, *, #9928, .F. ) ;
#10769=LINE ( 'NONE', #20267, #2680 ) ;
#10772=EDGE_LOOP ( 'NONE', ( #389, #1348, #1198 ) ) ;
#10774=LINE ( 'NONE', #18557, #7278 ) ;
#10775=CARTESIAN_POINT ( 'NONE',  ( 1.573500000000000343, 0.5250000000000000222, -0.1650000000000001465 ) ) ;
#10783=DIRECTION ( 'NONE',  ( 0.7071067811865514585, -1.056266077312799537E-17, -0.7071067811865436870 ) ) ;
#10787=FACE_OUTER_BOUND ( 'NONE', #10772, .T. ) ;
#10816=EDGE_CURVE ( 'NONE', #1066, #2961, #1103, .T. ) ;
#10819=VECTOR ( 'NONE', #19721, 39.37007874015748854 ) ;
#10821=ORIENTED_EDGE ( 'NONE', *, *, #3946, .F. ) ;
#10828=DIRECTION ( 'NONE',  ( 0.8660254037844361541, 0.000000000000000000, 0.5000000000000042188 ) ) ;
#10837=LINE ( 'NONE', #23982, #18323 ) ;
#10846=ORIENTED_EDGE ( 'NONE', *, *, #2081, .T. ) ;
#10850=CIRCLE ( 'NONE', #20950, 0.4624999999999992450 ) ;
#10874=ORIENTED_EDGE ( 'NONE', *, *, #9482, .T. ) ;
#10878=EDGE_CURVE ( 'NONE', #14303, #19328, #16345, .T. ) ;
#10912=EDGE_LOOP ( 'NONE', ( #18435, #1910, #19064, #6184 ) ) ;
#10913=ORIENTED_EDGE ( 'NONE', *, *, #20792, .T. ) ;
#10915=LINE ( 'NONE', #19935, #22397 ) ;
#10940=CARTESIAN_POINT ( 'NONE',  ( 1.573500000000000343, 0.5250000000000000222, -0.3524999999999999800 ) ) ;
#10945=VERTEX_POINT ( 'NONE', #20243 ) ;
#10947=CARTESIAN_POINT ( 'NONE',  ( 1.573500000000000343, 0.000000000000000000, -1.006250000000000311 ) ) ;
#10952=LINE ( 'NONE', #14486, #9310 ) ;
#10960=CARTESIAN_POINT ( 'NONE',  ( 0.3950000000000000178, 0.04999999999999921868, 1.768075471041792386E-33 ) ) ;
#10994=CARTESIAN_POINT ( 'NONE',  ( 0.5997114317030027841, 2.978485840173427324, -1.206013144887902788 ) ) ;
#10998=EDGE_CURVE ( 'NONE', #17107, #18221, #9749, .T. ) ;
#11004=FACE_OUTER_BOUND ( 'NONE', #16314, .T. ) ;
#11008=EDGE_CURVE ( 'NONE', #20991, #8464, #5598, .T. ) ;
#11013=CONICAL_SURFACE ( 'NONE', #7508, 0.2124999999999999944, 0.7853981633974463916 ) ;
#11014=EDGE_CURVE ( 'NONE', #10162, #12271, #17186, .T. ) ;
#11030=VECTOR ( 'NONE', #22494, 39.37007874015748854 ) ;
#11056=ORIENTED_EDGE ( 'NONE', *, *, #8365, .F. ) ;
#11066=ORIENTED_EDGE ( 'NONE', *, *, #906, .T. ) ;
#11073=FACE_OUTER_BOUND ( 'NONE', #4724, .T. ) ;
#11075=FACE_OUTER_BOUND ( 'NONE', #7365, .T. ) ;
#11080=FACE_OUTER_BOUND ( 'NONE', #9249, .T. ) ;
#11115=AXIS2_PLACEMENT_3D ( 'NONE', #11455, #6071, #9866 ) ;
#11117=EDGE_CURVE ( 'NONE', #18827, #5903, #15238, .T. ) ;
#11125=EDGE_LOOP ( 'NONE', ( #7342, #17646, #19538, #8095 ) ) ;
#11151=EDGE_CURVE ( 'NONE', #21943, #17107, #16939, .T. ) ;
#11152=ORIENTED_EDGE ( 'NONE', *, *, #5440, .T. ) ;
#11157=DIRECTION ( 'NONE',  ( -0.000000000000000000, -1.000000000000000000, 0.000000000000000000 ) ) ;
#11161=VERTEX_POINT ( 'NONE', #19016 ) ;
#11162=CARTESIAN_POINT ( 'NONE',  ( 1.573500000000000343, 2.683750000000000746, -1.006250000000000533 ) ) ;
#11164=CARTESIAN_POINT ( 'NONE',  ( 2.936000000000000387, 0.000000000000000000, -2.541000000000000369 ) ) ;
#11175=PLANE ( 'NONE',  #16275 ) ;
#11179=CARTESIAN_POINT ( 'NONE',  ( 0.3950000000000000178, 2.665000000000000036, -1.966000000000000192 ) ) ;
#11180=ORIENTED_EDGE ( 'NONE', *, *, #5457, .T. ) ;
#11189=DIRECTION ( 'NONE',  ( -0.4995222938423191095, -0.04370253788966848435, 0.8651979924482661177 ) ) ;
#11201=LINE ( 'NONE', #18631, #12060 ) ;
#11219=EDGE_CURVE ( 'NONE', #8072, #10945, #2548, .T. ) ;
#11228=ADVANCED_FACE ( 'NONE', ( #8142 ), #13891, .F. ) ;
#11232=VERTEX_POINT ( 'NONE', #10116 ) ;
#11237=CARTESIAN_POINT ( 'NONE',  ( 0.0005099541946469743911, 2.690509954194647335, -0.8851373192811128332 ) ) ;
#11256=CARTESIAN_POINT ( 'NONE',  ( 0.3950000000000000178, 2.665000000000000036, -2.591000000000000192 ) ) ;
#11263=DIRECTION ( 'NONE',  ( 0.000000000000000000, -1.000000000000000000, 0.000000000000000000 ) ) ;
#11270=ORIENTED_EDGE ( 'NONE', *, *, #8731, .F. ) ;
#11273=PLANE ( 'NONE',  #12412 ) ;
#11279=LINE ( 'NONE', #18348, #16422 ) ;
#11316=AXIS2_PLACEMENT_3D ( 'NONE', #2670, #17545, #9633 ) ;
#11318=LINE ( 'NONE', #14745, #20731 ) ;
#11321=VECTOR ( 'NONE', #20391, 39.37007874015748143 ) ;
#11331=AXIS2_PLACEMENT_3D ( 'NONE', #18633, #5823, #7537 ) ;
#11335=VERTEX_POINT ( 'NONE', #3501 ) ;
#11391=LINE ( 'NONE', #5775, #23549 ) ;
#11393=ORIENTED_EDGE ( 'NONE', *, *, #17932, .F. ) ;
#11395=ORIENTED_EDGE ( 'NONE', *, *, #18397, .T. ) ;
#11404=CARTESIAN_POINT ( 'NONE',  ( 0.4872114317030045716, 2.978485840173427324, -1.400868860739402422 ) ) ;
#11427=VECTOR ( 'NONE', #2035, 39.37007874015748143 ) ;
#11428=CARTESIAN_POINT ( 'NONE',  ( 1.020000000000000018, 2.740039370078740433, -2.591000000000000192 ) ) ;
#11441=DIRECTION ( 'NONE',  ( 0.5773502691896256200, -0.5773502691896257311, -0.5773502691896256200 ) ) ;
#11444=DIRECTION ( 'NONE',  ( 0.4472135954999560403, -0.4472135954999560403, 0.7745966692414856247 ) ) ;
#11455=CARTESIAN_POINT ( 'NONE',  ( 0.3949999999999999623, 2.978485840173427324, -0.04999999999999919092 ) ) ;
#11462=DIRECTION ( 'NONE',  ( 0.4254442446013927959, -0.6399207742898898044, -0.6399207742898944673 ) ) ;
#11478=AXIS2_PLACEMENT_3D ( 'NONE', #9835, #15441, #16902 ) ;
#11479=DIRECTION ( 'NONE',  ( -0.000000000000000000, -1.000000000000000000, -0.000000000000000000 ) ) ;
#11480=DIRECTION ( 'NONE',  ( 4.347502568299317526E-16, 0.7071067811865511255, 0.7071067811865439090 ) ) ;
#11488=AXIS2_PLACEMENT_3D ( 'NONE', #2362, #11631, #13591 ) ;
#11506=CARTESIAN_POINT ( 'NONE',  ( 0.2935666255429962290, 2.563566625542996302, -0.5657204318808580767 ) ) ;
#11514=CARTESIAN_POINT ( 'NONE',  ( 0.4872114317030045716, 2.291712385858714729, -1.340783969076326132 ) ) ;
#11528=CARTESIAN_POINT ( 'NONE',  ( 0.7919466436700954848, 2.665000000000000036, -2.986000000000000210 ) ) ;
#11545=ORIENTED_EDGE ( 'NONE', *, *, #1288, .F. ) ;
#11567=DIRECTION ( 'NONE',  ( 0.000000000000000000, -0.7071067811865514585, 0.7071067811865436870 ) ) ;
#11577=EDGE_LOOP ( 'NONE', ( #6570, #9867, #21757 ) ) ;
#11608=CARTESIAN_POINT ( 'NONE',  ( 2.352842711703412526, 2.664999999999999591, -2.591000000000000636 ) ) ;
#11611=LINE ( 'NONE', #13324, #9228 ) ;
#11626=CARTESIAN_POINT ( 'NONE',  ( 1.286352214327351806, 2.291712385858714285, -1.542360493909560759 ) ) ;
#11631=DIRECTION ( 'NONE',  ( 0.000000000000000000, -0.7071067811865475727, -0.7071067811865475727 ) ) ;
#11656=AXIS2_PLACEMENT_3D ( 'NONE', #7, #1971, #22450 ) ;
#11669=VECTOR ( 'NONE', #23359, 39.37007874015748143 ) ;
#11672=ADVANCED_FACE ( 'NONE', ( #5403 ), #24049, .F. ) ;
#11692=CARTESIAN_POINT ( 'NONE',  ( 2.361207924709802342, 0.006657555934166073386, -2.942657555934166780 ) ) ;
#11693=UNCERTAINTY_MEASURE_WITH_UNIT (LENGTH_MEASURE( 1.000000000000000082E-05 ), #9433, 'distance_accuracy_value', 'NONE');
#11715=ORIENTED_EDGE ( 'NONE', *, *, #13818, .T. ) ;
#11724=DIRECTION ( 'NONE',  ( -0.1474777632191348331, -0.6043296738907314447, -0.7829661260942282208 ) ) ;
#11732=ORIENTED_EDGE ( 'NONE', *, *, #4570, .T. ) ;
#11743=AXIS2_PLACEMENT_3D ( 'NONE', #24028, #9045, #5382 ) ;
#11748=DIRECTION ( 'NONE',  ( -0.3895442144046399879, 0.7839133596588501174, 0.4834616319546425900 ) ) ;
#11764=CARTESIAN_POINT ( 'NONE',  ( 0.9125529719201093126, 2.740000000000000213, -1.580588111963586062 ) ) ;
#11779=VERTEX_POINT ( 'NONE', #14809 ) ;
#11812=EDGE_CURVE ( 'NONE', #14200, #12633, #23770, .T. ) ;
#11818=VERTEX_POINT ( 'NONE', #13554 ) ;
#11829=CARTESIAN_POINT ( 'NONE',  ( 0.4959544880677846934, 2.765954488067785100, -0.6103003506586756055 ) ) ;
#11830=CARTESIAN_POINT ( 'NONE',  ( 0.5097595264191659981, 2.690047770615767941, -0.7016051277422445942 ) ) ;
#11850=CARTESIAN_POINT ( 'NONE',  ( 2.168722887430706070, 2.291712385858714729, -1.763529041877836212 ) ) ;
#11856=CARTESIAN_POINT ( 'NONE',  ( 0.000000000000000000, 2.740000000000000213, -2.516000000000000014 ) ) ;
#11864=LINE ( 'NONE', #17575, #20407 ) ;
#11869=ORIENTED_EDGE ( 'NONE', *, *, #22145, .F. ) ;
#11881=( NAMED_UNIT ( * ) SI_UNIT ( $, .STERADIAN. ) SOLID_ANGLE_UNIT ( ) );
#11885=CARTESIAN_POINT ( 'NONE',  ( 2.319244702705235195, 2.291712385858714729, -2.476240473580834323 ) ) ;
#11886=EDGE_CURVE ( 'NONE', #20229, #1066, #19379, .T. ) ;
#11888=ORIENTED_EDGE ( 'NONE', *, *, #14253, .F. ) ;
#11893=LINE ( 'NONE', #21262, #2743 ) ;
#11894=VECTOR ( 'NONE', #127, 39.37007874015748854 ) ;
#11897=ORIENTED_EDGE ( 'NONE', *, *, #1177, .F. ) ;
#11912=CARTESIAN_POINT ( 'NONE',  ( 0.000000000000000000, 2.740000000000000213, -2.936000000000001720 ) ) ;
#11913=DIRECTION ( 'NONE',  ( 0.000000000000000000, 0.000000000000000000, -1.000000000000000000 ) ) ;
#11926=CARTESIAN_POINT ( 'NONE',  ( 2.977666666666666906, 2.756666666666666821, -0.06666666666666686003 ) ) ;
#11928=LINE ( 'NONE', #2410, #9117 ) ;
#11943=AXIS2_PLACEMENT_3D ( 'NONE', #11404, #420, #22731 ) ;
#11954=DIRECTION ( 'NONE',  ( 0.8660254037844383745, 0.000000000000000000, 0.5000000000000004441 ) ) ;
#11968=ORIENTED_EDGE ( 'NONE', *, *, #14854, .F. ) ;
#11979=FACE_OUTER_BOUND ( 'NONE', #1764, .T. ) ;
#11997=VERTEX_POINT ( 'NONE', #19855 ) ;
#11998=VECTOR ( 'NONE', #7468, 39.37007874015748143 ) ;
#12031=ORIENTED_EDGE ( 'NONE', *, *, #8255, .T. ) ;
#12032=EDGE_CURVE ( 'NONE', #1184, #7614, #10601, .T. ) ;
#12041=EDGE_CURVE ( 'NONE', #21713, #19257, #7181, .T. ) ;
#12042=LINE ( 'NONE', #15914, #20084 ) ;
#12045=EDGE_LOOP ( 'NONE', ( #9108, #2444, #19689, #9208, #7862 ) ) ;
#12053=CARTESIAN_POINT ( 'NONE',  ( 2.356222887430696744, 2.291712385858714729, -2.088288568297006265 ) ) ;
#12060=VECTOR ( 'NONE', #1923, 39.37007874015748854 ) ;
#12065=CARTESIAN_POINT ( 'NONE',  ( 1.573500000000000343, 2.683750000000000746, -1.412500000000000089 ) ) ;
#12070=LINE ( 'NONE', #2665, #21700 ) ;
#12080=AXIS2_PLACEMENT_3D ( 'NONE', #8333, #2979, #10187 ) ;
#12083=DIRECTION ( 'NONE',  ( 1.000000000000000000, 0.000000000000000000, 0.000000000000000000 ) ) ;
#12086=ORIENTED_EDGE ( 'NONE', *, *, #12442, .T. ) ;
#12096=AXIS2_PLACEMENT_3D ( 'NONE', #21356, #13696, #6473 ) ;
#12109=ORIENTED_EDGE ( 'NONE', *, *, #10509, .F. ) ;
#12116=ORIENTED_EDGE ( 'NONE', *, *, #16978, .T. ) ;
#12123=CARTESIAN_POINT ( 'NONE',  ( 1.962866667188212455, 2.690142902515285428, -2.659351702128306183 ) ) ;
#12124=EDGE_CURVE ( 'NONE', #9581, #14200, #3881, .T. ) ;
#12126=DIRECTION ( 'NONE',  ( 0.8660254037844382635, 0.000000000000000000, 0.5000000000000007772 ) ) ;
#12127=ADVANCED_FACE ( 'NONE', ( #22530 ), #9371, .T. ) ;
#12133=DIRECTION ( 'NONE',  ( 0.3535533905932676246, -0.7071067811865477948, 0.6123724356957979120 ) ) ;
#12143=CARTESIAN_POINT ( 'NONE',  ( 1.973001146175420883, 2.291712385858714729, -1.876529041877832205 ) ) ;
#12167=ORIENTED_EDGE ( 'NONE', *, *, #23884, .T. ) ;
#12189=DIRECTION ( 'NONE',  ( 0.000000000000000000, 0.000000000000000000, -1.000000000000000000 ) ) ;
#12199=DIRECTION ( 'NONE',  ( 0.8660254037844382635, 0.000000000000000000, 0.5000000000000007772 ) ) ;
#12233=VERTEX_POINT ( 'NONE', #18592 ) ;
#12236=CARTESIAN_POINT ( 'NONE',  ( 2.040570600599760365, 0.000000000000000000, -2.386288568296997870 ) ) ;
#12241=VECTOR ( 'NONE', #20032, 39.37007874015748143 ) ;
#12247=VERTEX_POINT ( 'NONE', #24065 ) ;
#12255=CARTESIAN_POINT ( 'NONE',  ( 2.055580586463031434, 2.740000000000000213, -2.936000000000001720 ) ) ;
#12268=EDGE_LOOP ( 'NONE', ( #9275, #20851, #20900 ) ) ;
#12271=VERTEX_POINT ( 'NONE', #14826 ) ;
#12278=DIRECTION ( 'NONE',  ( -0.8651979924482662287, 0.04370253788966843578, 0.4995222938423188319 ) ) ;
#12290=DIRECTION ( 'NONE',  ( 0.7071067811865472397, -0.7071067811865476838, -4.229284785449151260E-16 ) ) ;
#12293=CIRCLE ( 'NONE', #14225, 0.4062499999999997780 ) ;
#12296=LINE ( 'NONE', #21423, #8165 ) ;
#12310=ADVANCED_FACE ( 'NONE', ( #17838 ), #21733, .T. ) ;
#12320=FACE_OUTER_BOUND ( 'NONE', #10643, .T. ) ;
#12322=DIRECTION ( 'NONE',  ( 0.000000000000000000, 0.9961946980917454342, -0.08715574274765830465 ) ) ;
#12335=LINE ( 'NONE', #19509, #6819 ) ;
#12341=CARTESIAN_POINT ( 'NONE',  ( 1.998815303304990465, 2.291712385858714729, -2.661240473580836152 ) ) ;
#12351=ORIENTED_EDGE ( 'NONE', *, *, #6308, .F. ) ;
#12355=ORIENTED_EDGE ( 'NONE', *, *, #2715, .F. ) ;
#12366=DIRECTION ( 'NONE',  ( 0.000000000000000000, -1.000000000000000000, 0.000000000000000000 ) ) ;
#12372=DIRECTION ( 'NONE',  ( 0.7071067811865475727, -0.7071067811865475727, 0.000000000000000000 ) ) ;
#12375=ADVANCED_FACE ( 'NONE', ( #1371 ), #14423, .T. ) ;
#12379=VECTOR ( 'NONE', #23197, 39.37007874015748854 ) ;
#12390=VERTEX_POINT ( 'NONE', #5137 ) ;
#12410=DIRECTION ( 'NONE',  ( -0.8635502596144366549, -0.07555085810113186529, -0.4985709748471343072 ) ) ;
#12412=AXIS2_PLACEMENT_3D ( 'NONE', #12760, #11157, #16759 ) ;
#12431=LINE ( 'NONE', #1560, #23896 ) ;
#12437=DIRECTION ( 'NONE',  ( 1.000000000000000000, -0.000000000000000000, 0.000000000000000000 ) ) ;
#12438=CARTESIAN_POINT ( 'NONE',  ( 1.020000000000000018, 2.665000000000000036, -2.591000000000000192 ) ) ;
#12442=EDGE_CURVE ( 'NONE', #17107, #20052, #3799, .T. ) ;
#12451=DIRECTION ( 'NONE',  ( 0.8660254037844434816, 0.000000000000000000, -0.4999999999999913403 ) ) ;
#12465=ORIENTED_EDGE ( 'NONE', *, *, #22587, .T. ) ;
#12470=ADVANCED_FACE ( 'NONE', ( #9164 ), #133, .T. ) ;
#12489=LINE ( 'NONE', #4909, #12725 ) ;
#12513=VECTOR ( 'NONE', #23755, 39.37007874015748143 ) ;
#12514=AXIS2_PLACEMENT_3D ( 'NONE', #15882, #14060, #21609 ) ;
#12518=VERTEX_POINT ( 'NONE', #7817 ) ;
#12539=EDGE_CURVE ( 'NONE', #544, #20226, #13686, .T. ) ;
#12553=DIRECTION ( 'NONE',  ( 0.000000000000000000, -0.5150380749100555988, -0.8571673007021114454 ) ) ;
#12582=LINE ( 'NONE', #17816, #18454 ) ;
#12588=ADVANCED_FACE ( 'NONE', ( #11979 ), #6583, .F. ) ;
#12591=DIRECTION ( 'NONE',  ( -0.5773502691896227335, -0.5773502691896255090, -0.5773502691896290617 ) ) ;
#12597=LINE ( 'NONE', #2453, #10763 ) ;
#12601=VECTOR ( 'NONE', #12322, 39.37007874015748143 ) ;
#12603=LINE ( 'NONE', #9046, #8108 ) ;
#12633=VERTEX_POINT ( 'NONE', #17684 ) ;
#12672=DIRECTION ( 'NONE',  ( 0.5773502691896236216, 0.5773502691896299499, -0.5773502691896236216 ) ) ;
#12676=CARTESIAN_POINT ( 'NONE',  ( 0.7919466436700954848, 2.665000000000000036, -2.986000000000000210 ) ) ;
#12685=CARTESIAN_POINT ( 'NONE',  ( 1.457716030923678074, 2.291712385858714729, -2.174029041877829194 ) ) ;
#12725=VECTOR ( 'NONE', #23547, 39.37007874015748143 ) ;
#12739=DIRECTION ( 'NONE',  ( 0.8660254037844524744, 0.000000000000000000, -0.4999999999999761857 ) ) ;
#12760=CARTESIAN_POINT ( 'NONE',  ( 3.025220084236446727, 2.291712385858714729, -2.986000000000001098 ) ) ;
#12761=ORIENTED_EDGE ( 'NONE', *, *, #11886, .F. ) ;
#12764=CARTESIAN_POINT ( 'NONE',  ( 0.4872114317030045716, 0.000000000000000000, -1.140285115251740145 ) ) ;
#12766=CARTESIAN_POINT ( 'NONE',  ( 2.986000000000000210, 0.05000000000000028727, -2.541000000000000369 ) ) ;
#12774=EDGE_CURVE ( 'NONE', #18008, #22560, #10143, .T. ) ;
#12785=ORIENTED_EDGE ( 'NONE', *, *, #6361, .T. ) ;
#12815=DIRECTION ( 'NONE',  ( -0.8651979924482607887, 0.04370253788966922681, 0.4995222938423283243 ) ) ;
#12826=ORIENTED_EDGE ( 'NONE', *, *, #1131, .T. ) ;
#12827=VERTEX_POINT ( 'NONE', #12942 ) ;
#12832=VECTOR ( 'NONE', #5422, 39.37007874015748854 ) ;
#12834=ORIENTED_EDGE ( 'NONE', *, *, #7686, .F. ) ;
#12851=ORIENTED_EDGE ( 'NONE', *, *, #14495, .T. ) ;
#12878=ORIENTED_EDGE ( 'NONE', *, *, #5216, .F. ) ;
#12889=DIRECTION ( 'NONE',  ( 0.5773502691896322814, -0.5773502691896258421, -0.5773502691896191807 ) ) ;
#12891=ORIENTED_EDGE ( 'NONE', *, *, #19918, .F. ) ;
#12921=ORIENTED_EDGE ( 'NONE', *, *, #22477, .T. ) ;
#12937=DIRECTION ( 'NONE',  ( -6.148297094540788948E-16, -1.493785812010397437E-17, -1.000000000000000000 ) ) ;
#12942=CARTESIAN_POINT ( 'NONE',  ( 1.020000000000000018, 0.05000000000000028727, -2.591000000000000192 ) ) ;
#12950=ORIENTED_EDGE ( 'NONE', *, *, #13032, .T. ) ;
#12996=ORIENTED_EDGE ( 'NONE', *, *, #776, .F. ) ;
#13000=CARTESIAN_POINT ( 'NONE',  ( 0.000000000000000000, 2.740000000000000213, -2.986000000000000210 ) ) ;
#13032=EDGE_CURVE ( 'NONE', #8464, #19892, #19569, .T. ) ;
#13048=DIRECTION ( 'NONE',  ( -0.000000000000000000, 0.9961946980917454342, -0.08715574274765824914 ) ) ;
#13053=ADVANCED_FACE ( 'NONE', ( #5173 ), #10675, .T. ) ;
#13055=AXIS2_PLACEMENT_3D ( 'NONE', #2216, #11480, #6218 ) ;
#13057=EDGE_CURVE ( 'NONE', #7051, #20991, #3469, .T. ) ;
#13063=DIRECTION ( 'NONE',  ( 0.8660254037844434816, -0.000000000000000000, -0.4999999999999915068 ) ) ;
#13076=DIRECTION ( 'NONE',  ( 1.707404996040164512E-16, 0.000000000000000000, -1.000000000000000000 ) ) ;
#13079=VECTOR ( 'NONE', #18761, 39.37007874015748854 ) ;
#13083=EDGE_CURVE ( 'NONE', #6253, #11779, #19907, .T. ) ;
#13098=VECTOR ( 'NONE', #984, 39.37007874015748143 ) ;
#13101=DIRECTION ( 'NONE',  ( 0.4999999999999909517, -0.000000000000000000, -0.8660254037844438146 ) ) ;
#13104=LINE ( 'NONE', #18442, #11998 ) ;
#13116=ORIENTED_EDGE ( 'NONE', *, *, #21874, .F. ) ;
#13122=DIRECTION ( 'NONE',  ( 0.000000000000000000, -0.7071067811865475727, 0.7071067811865475727 ) ) ;
#13126=LINE ( 'NONE', #2122, #23785 ) ;
#13139=DIRECTION ( 'NONE',  ( 1.000000000000000000, 0.000000000000000000, -0.000000000000000000 ) ) ;
#13143=DIRECTION ( 'NONE',  ( -0.3535533905932761733, -0.7071067811865487940, 0.6123724356957918058 ) ) ;
#13146=LINE ( 'NONE', #69, #190 ) ;
#13167=VECTOR ( 'NONE', #5030, 39.37007874015748143 ) ;
#13179=DIRECTION ( 'NONE',  ( -0.8660254037844434816, -2.725147086360870403E-18, 0.4999999999999913403 ) ) ;
#13194=DIRECTION ( 'NONE',  ( -0.000000000000000000, -1.000000000000000000, -0.000000000000000000 ) ) ;
#13200=EDGE_CURVE ( 'NONE', #8250, #11335, #13126, .T. ) ;
#13202=CARTESIAN_POINT ( 'NONE',  ( 1.573500000000000343, -3.414809992080329023E-17, -1.412500000000000089 ) ) ;
#13222=EDGE_CURVE ( 'NONE', #2181, #11779, #16878, .T. ) ;
#13227=DIRECTION ( 'NONE',  ( -0.8660254037844433705, 0.000000000000000000, 0.4999999999999917843 ) ) ;
#13232=VECTOR ( 'NONE', #11444, 39.37007874015748854 ) ;
#13236=EDGE_CURVE ( 'NONE', #21079, #20226, #11279, .T. ) ;
#13237=CARTESIAN_POINT ( 'NONE',  ( 2.936000000000001720, 2.740000000000000213, -2.516000000000000014 ) ) ;
#13239=VERTEX_POINT ( 'NONE', #169 ) ;
#13246=ORIENTED_EDGE ( 'NONE', *, *, #13947, .F. ) ;
#13249=ORIENTED_EDGE ( 'NONE', *, *, #16183, .F. ) ;
#13254=FACE_OUTER_BOUND ( 'NONE', #17750, .T. ) ;
#13265=ORIENTED_EDGE ( 'NONE', *, *, #14761, .T. ) ;
#13280=LINE ( 'NONE', #10454, #1181 ) ;
#13305=CARTESIAN_POINT ( 'NONE',  ( 0.3247595264191642794, 2.291712385858714729, -0.9871846966950100777 ) ) ;
#13317=DIRECTION ( 'NONE',  ( -0.4999999999999912292, 0.000000000000000000, 0.8660254037844437036 ) ) ;
#13322=ORIENTED_EDGE ( 'NONE', *, *, #10070, .F. ) ;
#13324=CARTESIAN_POINT ( 'NONE',  ( 0.4116666666666667918, 2.681666666666666643, -2.557666666666666533 ) ) ;
#13330=PLANE ( 'NONE',  #14824 ) ;
#13338=CARTESIAN_POINT ( 'NONE',  ( 1.573500000000000343, 2.683750000000000746, -1.412500000000000089 ) ) ;
#13341=CARTESIAN_POINT ( 'NONE',  ( 1.840071746775174377, 2.291712385858714285, -2.386288568296996981 ) ) ;
#13344=EDGE_CURVE ( 'NONE', #1661, #13614, #3586, .T. ) ;
#13346=ORIENTED_EDGE ( 'NONE', *, *, #10509, .T. ) ;
#13349=PLANE ( 'NONE',  #17721 ) ;
#13354=DIRECTION ( 'NONE',  ( 0.000000000000000000, 0.7071067811865474617, 0.7071067811865474617 ) ) ;
#13395=CARTESIAN_POINT ( 'NONE',  ( 0.000000000000000000, 2.740000000000000213, -2.936000000000001720 ) ) ;
#13403=ORIENTED_EDGE ( 'NONE', *, *, #5906, .T. ) ;
#13413=LINE ( 'NONE', #17539, #810 ) ;
#13420=LINE ( 'NONE', #20841, #14433 ) ;
#13459=B_SPLINE_CURVE_WITH_KNOTS ( 'NONE', 3,
 ( #18628, #18385, #9113, #21799, #16563, #24105, #14866, #20459, #3756, #16202, #7885, #18750, #15217, #571, #9728, #16807, #22402, #9608 ),
 .UNSPECIFIED., .F., .F.,
 ( 4, 2, 2, 2, 2, 2, 2, 2, 4 ),
 ( 6.938893903907228378E-18, 0.001843124596548163753, 0.003686249193096320566, 0.005529373789644477163, 0.007372498386192625520, 0.009215622982740773877, 0.01105874757928892137, 0.01290187217583707233, 0.01474499677238521808 ),
 .UNSPECIFIED. ) ;
#13463=PLANE ( 'NONE',  #23065 ) ;
#13470=CARTESIAN_POINT ( 'NONE',  ( 1.573500000000000343, -3.414809992080329023E-17, -0.9499999999999999556 ) ) ;
#13482=LINE ( 'NONE', #11764, #21021 ) ;
#13494=VECTOR ( 'NONE', #1607, 39.37007874015748143 ) ;
#13499=ORIENTED_EDGE ( 'NONE', *, *, #13222, .T. ) ;
#13504=ORIENTED_EDGE ( 'NONE', *, *, #15332, .F. ) ;
#13507=CARTESIAN_POINT ( 'NONE',  ( 0.5097595264191665532, 2.291712385858714285, -0.6667552972947643486 ) ) ;
#13529=DIRECTION ( 'NONE',  ( 0.000000000000000000, -0.7071067811865475727, -0.7071067811865475727 ) ) ;
#13553=DIRECTION ( 'NONE',  ( -0.5773502691896257311, -0.5773502691896257311, 0.5773502691896258421 ) ) ;
#13554=CARTESIAN_POINT ( 'NONE',  ( 0.3228432657101673042, 2.690047770615767941, -1.025353588051019837 ) ) ;
#13557=EDGE_LOOP ( 'NONE', ( #3104, #7609, #10438, #105, #527 ) ) ;
#13571=CARTESIAN_POINT ( 'NONE',  ( 0.7919466436700954848, 2.665000000000000036, -2.986000000000000210 ) ) ;
#13591=DIRECTION ( 'NONE',  ( 1.000000000000000000, 0.000000000000000000, 0.000000000000000000 ) ) ;
#13594=CARTESIAN_POINT ( 'NONE',  ( 2.316810681416314743, 2.319533376497107557, -2.476240473580834323 ) ) ;
#13596=EDGE_LOOP ( 'NONE', ( #5883, #15462, #2988, #11393 ) ) ;
#13610=CARTESIAN_POINT ( 'NONE',  ( 0.8977114317029943891, 2.978485840173427324, -0.6898620042323803103 ) ) ;
#13614=VERTEX_POINT ( 'NONE', #14181 ) ;
#13616=ORIENTED_EDGE ( 'NONE', *, *, #8365, .T. ) ;
#13618=VERTEX_POINT ( 'NONE', #19909 ) ;
#13619=ORIENTED_EDGE ( 'NONE', *, *, #15409, .T. ) ;
#13639=LINE ( 'NONE', #2529, #23832 ) ;
#13653=EDGE_CURVE ( 'NONE', #14487, #8144, #19365, .T. ) ;
#13654=CARTESIAN_POINT ( 'NONE',  ( 1.573500000000000343, -3.414809992080329023E-17, -0.3524999999999999800 ) ) ;
#13655=ORIENTED_EDGE ( 'NONE', *, *, #12032, .T. ) ;
#13658=VECTOR ( 'NONE', #13063, 39.37007874015748854 ) ;
#13662=CARTESIAN_POINT ( 'NONE',  ( 2.319244702705235195, 2.291712385858714729, -2.476240473580834323 ) ) ;
#13665=EDGE_LOOP ( 'NONE', ( #20727, #16252, #6249, #8597, #13619 ) ) ;
#13686=LINE ( 'NONE', #21103, #815 ) ;
#13696=DIRECTION ( 'NONE',  ( 0.7071067811865451302, -0.06162841671621964446, -0.7044160264027610197 ) ) ;
#13704=ORIENTED_EDGE ( 'NONE', *, *, #23443, .T. ) ;
#13707=CARTESIAN_POINT ( 'NONE',  ( 2.159030003005114828, 2.291712385858714285, -2.568740473580834127 ) ) ;
#13709=ORIENTED_EDGE ( 'NONE', *, *, #15962, .F. ) ;
#13720=FACE_OUTER_BOUND ( 'NONE', #16106, .T. ) ;
#13721=EDGE_LOOP ( 'NONE', ( #21471, #18196, #2854, #3712 ) ) ;
#13735=VERTEX_POINT ( 'NONE', #19698 ) ;
#13758=DIRECTION ( 'NONE',  ( -0.8660254037844434816, 0.000000000000000000, -0.4999999999999913403 ) ) ;
#13759=ORIENTED_EDGE ( 'NONE', *, *, #19301, .T. ) ;
#13765=CARTESIAN_POINT ( 'NONE',  ( 1.573500000000000343, 0.05625000000000004996, -1.412500000000000089 ) ) ;
#13788=PLANE ( 'NONE',  #7966 ) ;
#13795=AXIS2_PLACEMENT_3D ( 'NONE', #1471, #6837, #5237 ) ;
#13801=LINE ( 'NONE', #21232, #13098 ) ;
#13817=LINE ( 'NONE', #17347, #16920 ) ;
#13818=EDGE_CURVE ( 'NONE', #16523, #20947, #1350, .T. ) ;
#13824=ORIENTED_EDGE ( 'NONE', *, *, #5188, .F. ) ;
#13830=AXIS2_PLACEMENT_3D ( 'NONE', #19923, #9061, #17976 ) ;
#13839=CARTESIAN_POINT ( 'NONE',  ( 0.5097595264191659981, 2.291712385858714729, -0.6667552972947653478 ) ) ;
#13876=CARTESIAN_POINT ( 'NONE',  ( 0.3950000000000000178, 2.978485840173427324, -0.2605837454876624437 ) ) ;
#13891=PLANE ( 'NONE',  #17947 ) ;
#13893=ORIENTED_EDGE ( 'NONE', *, *, #5457, .F. ) ;
#13894=DIRECTION ( 'NONE',  ( -0.8660254037844434816, -0.000000000000000000, 0.4999999999999914513 ) ) ;
#13901=DIRECTION ( 'NONE',  ( 0.4999999999999912292, 0.000000000000000000, -0.8660254037844437036 ) ) ;
#13902=CARTESIAN_POINT ( 'NONE',  ( 1.779986855112097865, 2.978485840173427324, -2.386288568296997870 ) ) ;
#13903=DIRECTION ( 'NONE',  ( 0.000000000000000000, 0.000000000000000000, 1.000000000000000000 ) ) ;
#13909=LINE ( 'NONE', #22801, #4470 ) ;
#13911=CARTESIAN_POINT ( 'NONE',  ( 0.4700000000000002509, 2.740000000000000213, -0.6252851813312900742 ) ) ;
#13925=EDGE_LOOP ( 'NONE', ( #16040, #2607, #821, #11732 ) ) ;
#13936=CIRCLE ( 'NONE', #15472, 0.1874999999999998335 ) ;
#13937=DIRECTION ( 'NONE',  ( 1.707404996040164512E-16, 0.000000000000000000, -1.000000000000000000 ) ) ;
#13943=VERTEX_POINT ( 'NONE', #8781 ) ;
#13944=PLANE ( 'NONE',  #5792 ) ;
#13947=EDGE_CURVE ( 'NONE', #14330, #9147, #23406, .T. ) ;
#13966=VECTOR ( 'NONE', #19936, 39.37007874015748854 ) ;
#13970=CARTESIAN_POINT ( 'NONE',  ( 0.4336681474472749986, 3.704141657475161331, -2.371204961265731104 ) ) ;
#13978=AXIS2_PLACEMENT_3D ( 'NONE', #18315, #7104, #3676 ) ;
#13983=LINE ( 'NONE', #6412, #3864 ) ;
#14006=ORIENTED_EDGE ( 'NONE', *, *, #23418, .F. ) ;
#14016=LINE ( 'NONE', #17914, #15135 ) ;
#14018=DIRECTION ( 'NONE',  ( 0.2492442549762389770, 0.5597738724868880356, -0.7902724296357380718 ) ) ;
#14021=ORIENTED_EDGE ( 'NONE', *, *, #18698, .F. ) ;
#14029=AXIS2_PLACEMENT_3D ( 'NONE', #23352, #8487, #13758 ) ;
#14060=DIRECTION ( 'NONE',  ( 0.5643569814744680002, 0.7585083585221992220, 0.3258316551733211330 ) ) ;
#14062=ORIENTED_EDGE ( 'NONE', *, *, #1736, .F. ) ;
#14064=VECTOR ( 'NONE', #18030, 39.37007874015748854 ) ;
#14072=CARTESIAN_POINT ( 'NONE',  ( 1.964916176665831848, 2.661358883302036293, -1.862525463909579626 ) ) ;
#14074=DIRECTION ( 'NONE',  ( 0.5773502691896215122, 0.5773502691896279515, 0.5773502691896278405 ) ) ;
#14083=EDGE_LOOP ( 'NONE', ( #23370, #5627, #14585, #8079 ) ) ;
#14085=EDGE_LOOP ( 'NONE', ( #12465, #3952, #12878, #9266 ) ) ;
#14089=LINE ( 'NONE', #8600, #13966 ) ;
#14091=DIRECTION ( 'NONE',  ( -0.000000000000000000, -1.000000000000000000, -0.000000000000000000 ) ) ;
#14093=PLANE ( 'NONE',  #1897 ) ;
#14095=EDGE_LOOP ( 'NONE', ( #3738, #21275, #15996, #13246, #19535 ) ) ;
#14096=LINE ( 'NONE', #6898, #20854 ) ;
#14103=DIRECTION ( 'NONE',  ( -0.000000000000000000, -1.000000000000000000, -0.000000000000000000 ) ) ;
#14121=FACE_OUTER_BOUND ( 'NONE', #18554, .T. ) ;
#14127=LINE ( 'NONE', #14248, #16855 ) ;
#14134=CARTESIAN_POINT ( 'NONE',  ( 1.573500000000000343, 2.683750000000000746, -1.412500000000000089 ) ) ;
#14156=ORIENTED_EDGE ( 'NONE', *, *, #21540, .F. ) ;
#14159=DIRECTION ( 'NONE',  ( 0.5773502691896256200, 0.5773502691896259531, 0.5773502691896256200 ) ) ;
#14167=ORIENTED_EDGE ( 'NONE', *, *, #14489, .F. ) ;
#14180=ORIENTED_EDGE ( 'NONE', *, *, #18271, .T. ) ;
#14181=CARTESIAN_POINT ( 'NONE',  ( 2.361000000000004206, 0.000000000000000000, -2.201288568297000925 ) ) ;
#14200=VERTEX_POINT ( 'NONE', #4371 ) ;
#14222=LINE ( 'NONE', #2874, #15115 ) ;
#14225=AXIS2_PLACEMENT_3D ( 'NONE', #9132, #20474, #3770 ) ;
#14238=EDGE_CURVE ( 'NONE', #363, #6320, #6201, .T. ) ;
#14244=ORIENTED_EDGE ( 'NONE', *, *, #19446, .F. ) ;
#14248=CARTESIAN_POINT ( 'NONE',  ( 2.556721741255282954, 0.000000000000000000, -2.088288568297006265 ) ) ;
#14252=PLANE ( 'NONE',  #9714 ) ;
#14253=EDGE_CURVE ( 'NONE', #7960, #1032, #1960, .T. ) ;
#14276=ORIENTED_EDGE ( 'NONE', *, *, #16478, .F. ) ;
#14289=FACE_OUTER_BOUND ( 'NONE', #17475, .T. ) ;
#14303=VERTEX_POINT ( 'NONE', #18899 ) ;
#14306=DIRECTION ( 'NONE',  ( 0.000000000000000000, 0.000000000000000000, 1.000000000000000000 ) ) ;
#14312=VECTOR ( 'NONE', #20034, 39.37007874015748143 ) ;
#14324=EDGE_CURVE ( 'NONE', #16427, #363, #13420, .T. ) ;
#14330=VERTEX_POINT ( 'NONE', #19020 ) ;
#14342=DIRECTION ( 'NONE',  ( 0.000000000000000000, -0.7071067811865489050, -0.7071067811865461294 ) ) ;
#14367=DIRECTION ( 'NONE',  ( -1.707404996040164512E-16, 0.000000000000000000, 1.000000000000000000 ) ) ;
#14372=DIRECTION ( 'NONE',  ( -0.6568875074630621258, 0.6516633103466551447, -0.3792541792610923390 ) ) ;
#14381=EDGE_CURVE ( 'NONE', #12247, #18827, #15830, .T. ) ;
#14407=ORIENTED_EDGE ( 'NONE', *, *, #16857, .F. ) ;
#14421=ORIENTED_EDGE ( 'NONE', *, *, #16816, .T. ) ;
#14423=PLANE ( 'NONE',  #1985 ) ;
#14429=FACE_OUTER_BOUND ( 'NONE', #20246, .T. ) ;
#14433=VECTOR ( 'NONE', #6081, 39.37007874015748854 ) ;
#14452=ORIENTED_EDGE ( 'NONE', *, *, #17932, .T. ) ;
#14460=CARTESIAN_POINT ( 'NONE',  ( 1.573500000000000343, 2.740000000000000213, -1.412500000000000089 ) ) ;
#14473=AXIS2_PLACEMENT_3D ( 'NONE', #14460, #14091, #1163 ) ;
#14478=CARTESIAN_POINT ( 'NONE',  ( 0.4872114317030045716, 0.000000000000000000, -1.140285115251740145 ) ) ;
#14486=CARTESIAN_POINT ( 'NONE',  ( 1.573500000000000343, 0.000000000000000000, -1.818749999999999867 ) ) ;
#14487=VERTEX_POINT ( 'NONE', #5576 ) ;
#14489=EDGE_CURVE ( 'NONE', #22355, #20229, #23852, .T. ) ;
#14491=CARTESIAN_POINT ( 'NONE',  ( 2.159030003005114828, 2.291712385858714285, -2.568740473580834127 ) ) ;
#14492=DIRECTION ( 'NONE',  ( 0.000000000000000000, -1.000000000000000000, 1.493785812010397437E-17 ) ) ;
#14495=EDGE_CURVE ( 'NONE', #12271, #12827, #10837, .T. ) ;
#14520=ORIENTED_EDGE ( 'NONE', *, *, #14324, .T. ) ;
#14528=AXIS2_PLACEMENT_3D ( 'NONE', #13338, #9426, #4051 ) ;
#14548=CARTESIAN_POINT ( 'NONE',  ( -1.546911548986461295E-15, 2.740000000000000213, -2.515999999999997794 ) ) ;
#14569=VERTEX_POINT ( 'NONE', #9483 ) ;
#14575=PLANE ( 'NONE',  #4220 ) ;
#14576=ORIENTED_EDGE ( 'NONE', *, *, #16946, .F. ) ;
#14581=LINE ( 'NONE', #20421, #20470 ) ;
#14585=ORIENTED_EDGE ( 'NONE', *, *, #13236, .F. ) ;
#14595=EDGE_CURVE ( 'NONE', #24062, #544, #13280, .T. ) ;
#14599=AXIS2_PLACEMENT_3D ( 'NONE', #21665, #18011, #6912 ) ;
#14611=VECTOR ( 'NONE', #13179, 39.37007874015748854 ) ;
#14626=ORIENTED_EDGE ( 'NONE', *, *, #16172, .F. ) ;
#14629=VECTOR ( 'NONE', #14701, 39.37007874015748143 ) ;
#14630=DIRECTION ( 'NONE',  ( -0.000000000000000000, -1.000000000000000000, -0.000000000000000000 ) ) ;
#14654=DIRECTION ( 'NONE',  ( 0.000000000000000000, 0.000000000000000000, -1.000000000000000000 ) ) ;
#14661=DIRECTION ( 'NONE',  ( 0.7745966692414850696, -0.4472135954999565954, 0.4472135954999565954 ) ) ;
#14672=ORIENTED_EDGE ( 'NONE', *, *, #19643, .F. ) ;
#14700=DIRECTION ( 'NONE',  ( -0.4999999999999913403, 0.000000000000000000, 0.8660254037844437036 ) ) ;
#14701=DIRECTION ( 'NONE',  ( 0.000000000000000000, 0.000000000000000000, 1.000000000000000000 ) ) ;
#14702=FACE_OUTER_BOUND ( 'NONE', #5851, .T. ) ;
#14711=ORIENTED_EDGE ( 'NONE', *, *, #1288, .T. ) ;
#14714=LINE ( 'NONE', #16288, #23961 ) ;
#14733=EDGE_CURVE ( 'NONE', #19306, #4696, #19299, .T. ) ;
#14735=AXIS2_PLACEMENT_3D ( 'NONE', #15223, #13529, #2415 ) ;
#14736=ORIENTED_EDGE ( 'NONE', *, *, #13236, .T. ) ;
#14745=CARTESIAN_POINT ( 'NONE',  ( 1.397631139260601341, 2.978485840173427324, -2.174029041877829638 ) ) ;
#14754=ORIENTED_EDGE ( 'NONE', *, *, #2472, .T. ) ;
#14761=EDGE_CURVE ( 'NONE', #14781, #3473, #6126, .T. ) ;
#14781=VERTEX_POINT ( 'NONE', #13594 ) ;
#14802=CARTESIAN_POINT ( 'NONE',  ( 1.011880822804989588, 2.476536290232590698, -1.198199922892767333 ) ) ;
#14809=CARTESIAN_POINT ( 'NONE',  ( 1.573500000000000343, 2.740000000000000213, -0.9500000000000008438 ) ) ;
#14821=DIRECTION ( 'NONE',  ( 0.000000000000000000, 1.000000000000000000, -1.493785812010397437E-17 ) ) ;
#14824=AXIS2_PLACEMENT_3D ( 'NONE', #15271, #3931, #20515 ) ;
#14826=CARTESIAN_POINT ( 'NONE',  ( 0.7919466436700954848, 0.05000000000000028727, -2.986000000000000210 ) ) ;
#14832=ORIENTED_EDGE ( 'NONE', *, *, #16291, .T. ) ;
#14845=DIRECTION ( 'NONE',  ( 0.8660254037844361541, 0.000000000000000000, 0.5000000000000042188 ) ) ;
#14854=EDGE_CURVE ( 'NONE', #1954, #5136, #8772, .T. ) ;
#14865=CARTESIAN_POINT ( 'NONE',  ( 2.160501146175418441, 2.291712385858714729, -2.201288568297000925 ) ) ;
#14866=CARTESIAN_POINT ( 'NONE',  ( 1.889965290469428183, 2.453197021783230181, -1.916312967630974695 ) ) ;
#14874=VERTEX_POINT ( 'NONE', #235 ) ;
#14878=LINE ( 'NONE', #18519, #14611 ) ;
#14913=VECTOR ( 'NONE', #2173, 39.37007874015748854 ) ;
#14917=CARTESIAN_POINT ( 'NONE',  ( 1.047989435620467535, 2.471736157945124912, -1.135238013746948438 ) ) ;
#14953=CARTESIAN_POINT ( 'NONE',  ( 0.000000000000000000, 2.740000000000000213, 0.000000000000000000 ) ) ;
#14967=DIRECTION ( 'NONE',  ( -0.000000000000000000, -1.000000000000000000, -0.000000000000000000 ) ) ;
#14979=FACE_OUTER_BOUND ( 'NONE', #15917, .T. ) ;
#14983=VECTOR ( 'NONE', #22473, 39.37007874015748854 ) ;
#14994=EDGE_CURVE ( 'NONE', #14330, #6883, #13413, .T. ) ;
#15002=DIRECTION ( 'NONE',  ( 0.08715574274765830465, -0.9961946980917454342, -3.870492493070289564E-17 ) ) ;
#15021=CARTESIAN_POINT ( 'NONE',  ( 1.962795215930568826, 2.690142902515285428, -2.659227944919802855 ) ) ;
#15027=ORIENTED_EDGE ( 'NONE', *, *, #7686, .T. ) ;
#15028=ORIENTED_EDGE ( 'NONE', *, *, #23584, .F. ) ;
#15053=ORIENTED_EDGE ( 'NONE', *, *, #11151, .F. ) ;
#15062=DIRECTION ( 'NONE',  ( -0.8660254037844438146, -0.000000000000000000, -0.4999999999999910627 ) ) ;
#15068=ORIENTED_EDGE ( 'NONE', *, *, #22587, .F. ) ;
#15069=LINE ( 'NONE', #22491, #15367 ) ;
#15072=LINE ( 'NONE', #7857, #23083 ) ;
#15079=PLANE ( 'NONE',  #22962 ) ;
#15082=ORIENTED_EDGE ( 'NONE', *, *, #16857, .T. ) ;
#15091=EDGE_LOOP ( 'NONE', ( #3085, #23128, #5486, #9861, #9966, #5411, #22314 ) ) ;
#15115=VECTOR ( 'NONE', #12290, 39.37007874015748854 ) ;
#15123=DIRECTION ( 'NONE',  ( 0.4999999999999912292, -2.725147086360871558E-18, -0.8660254037844437036 ) ) ;
#15135=VECTOR ( 'NONE', #21688, 39.37007874015748143 ) ;
#15165=VECTOR ( 'NONE', #23440, 39.37007874015748143 ) ;
#15166=CARTESIAN_POINT ( 'NONE',  ( 0.3950000000000000178, 2.665000000000000036, -2.540999999999999925 ) ) ;
#15167=ORIENTED_EDGE ( 'NONE', *, *, #16032, .F. ) ;
#15170=DIRECTION ( 'NONE',  ( 0.3993784937532309232, -0.7060941387255963431, -0.5847460012558945985 ) ) ;
#15179=FACE_OUTER_BOUND ( 'NONE', #16131, .T. ) ;
#15194=ORIENTED_EDGE ( 'NONE', *, *, #11117, .T. ) ;
#15217=CARTESIAN_POINT ( 'NONE',  ( 1.711101542529408048, 2.439517176785165109, -2.020270991558039242 ) ) ;
#15220=VECTOR ( 'NONE', #15123, 39.37007874015748143 ) ;
#15223=CARTESIAN_POINT ( 'NONE',  ( 1.020000000000000018, 0.05000000000000028727, -2.591000000000000192 ) ) ;
#15238=LINE ( 'NONE', #22667, #8596 ) ;
#15264=ORIENTED_EDGE ( 'NONE', *, *, #59, .F. ) ;
#15271=CARTESIAN_POINT ( 'NONE',  ( 0.7919466436700954848, 2.740039370078740433, -2.986000000000000210 ) ) ;
#15284=ORIENTED_EDGE ( 'NONE', *, *, #10816, .T. ) ;
#15324=CARTESIAN_POINT ( 'NONE',  ( 1.149903810567666440, 2.740000000000000213, -2.516000000000000014 ) ) ;
#15332=EDGE_CURVE ( 'NONE', #20123, #1661, #23198, .T. ) ;
#15336=LINE ( 'NONE', #570, #2819 ) ;
#15337=PLANE ( 'NONE',  #1835 ) ;
#15342=CARTESIAN_POINT ( 'NONE',  ( 9.065143943205062133E-18, 0.05000000000000028727, -2.194053356329904947 ) ) ;
#15348=CARTESIAN_POINT ( 'NONE',  ( 1.573500000000000343, -3.414809992080329023E-17, -0.5649999999999999467 ) ) ;
#15365=DIRECTION ( 'NONE',  ( -0.8651979924482607887, 0.04370253788966922681, 0.4995222938423283243 ) ) ;
#15367=VECTOR ( 'NONE', #22320, 39.37007874015748143 ) ;
#15375=ADVANCED_FACE ( 'NONE', ( #8451 ), #3998, .T. ) ;
#15377=FACE_OUTER_BOUND ( 'NONE', #23570, .T. ) ;
#15394=ORIENTED_EDGE ( 'NONE', *, *, #22270, .F. ) ;
#15400=DIRECTION ( 'NONE',  ( 0.3266093577730910247, -0.7067687497613774905, 0.6275382552289447968 ) ) ;
#15406=VERTEX_POINT ( 'NONE', #4557 ) ;
#15409=EDGE_CURVE ( 'NONE', #5661, #20947, #10060, .T. ) ;
#15420=ORIENTED_EDGE ( 'NONE', *, *, #23620, .F. ) ;
#15426=LINE ( 'NONE', #13610, #9863 ) ;
#15441=DIRECTION ( 'NONE',  ( 0.7071067811865475727, 0.000000000000000000, 0.7071067811865475727 ) ) ;
#15442=DIRECTION ( 'NONE',  ( -0.000000000000000000, -1.000000000000000000, -0.000000000000000000 ) ) ;
#15462=ORIENTED_EDGE ( 'NONE', *, *, #10383, .F. ) ;
#15472=AXIS2_PLACEMENT_3D ( 'NONE', #21550, #19243, #2547 ) ;
#15475=LINE ( 'NONE', #7550, #4152 ) ;
#15504=CARTESIAN_POINT ( 'NONE',  ( 1.998815303304994018, 2.291712385858714285, -2.661240473580833488 ) ) ;
#15517=CARTESIAN_POINT ( 'NONE',  ( 1.652571746775178152, 2.291712385858714285, -2.061529041877830704 ) ) ;
#15535=FACE_OUTER_BOUND ( 'NONE', #8027, .T. ) ;
#15549=ORIENTED_EDGE ( 'NONE', *, *, #2915, .T. ) ;
#15552=ORIENTED_EDGE ( 'NONE', *, *, #19918, .T. ) ;
#15557=AXIS2_PLACEMENT_3D ( 'NONE', #22770, #95, #19114 ) ;
#15566=ORIENTED_EDGE ( 'NONE', *, *, #3366, .F. ) ;
#15573=LINE ( 'NONE', #10456, #18997 ) ;
#15576=EDGE_CURVE ( 'NONE', #9147, #23278, #4614, .T. ) ;
#15607=FACE_OUTER_BOUND ( 'NONE', #14085, .T. ) ;
#15615=VECTOR ( 'NONE', #1489, 39.37007874015748854 ) ;
#15618=FACE_OUTER_BOUND ( 'NONE', #7916, .T. ) ;
#15619=DIRECTION ( 'NONE',  ( 1.000000000000000000, 0.000000000000000000, -6.148297094540788948E-16 ) ) ;
#15629=PLANE ( 'NONE',  #23494 ) ;
#15643=LINE ( 'NONE', #15763, #15762 ) ;
#15658=CARTESIAN_POINT ( 'NONE',  ( 1.846908021952178069, 1.442300479962384641, -4.378300479962384806 ) ) ;
#15660=CARTESIAN_POINT ( 'NONE',  ( 1.990666666666680795, -0.9453333333333302502, -0.9953333333333292954 ) ) ;
#15662=FACE_OUTER_BOUND ( 'NONE', #5652, .T. ) ;
#15665=ORIENTED_EDGE ( 'NONE', *, *, #18696, .F. ) ;
#15670=ORIENTED_EDGE ( 'NONE', *, *, #4570, .F. ) ;
#15673=ORIENTED_EDGE ( 'NONE', *, *, #5401, .T. ) ;
#15698=VERTEX_POINT ( 'NONE', #11830 ) ;
#15701=EDGE_LOOP ( 'NONE', ( #638, #23064, #17674, #4247 ) ) ;
#15732=EDGE_CURVE ( 'NONE', #11161, #1661, #14127, .T. ) ;
#15733=ADVANCED_FACE ( 'NONE', ( #17907 ), #4762, .F. ) ;
#15751=FACE_OUTER_BOUND ( 'NONE', #13596, .T. ) ;
#15757=DIRECTION ( 'NONE',  ( -0.000000000000000000, -0.9961946980917454342, 0.08715574274765830465 ) ) ;
#15762=VECTOR ( 'NONE', #23060, 39.37007874015748854 ) ;
#15763=CARTESIAN_POINT ( 'NONE',  ( 1.222470958122163998, 2.291712385858714729, -0.8172771125692949168 ) ) ;
#15764=ORIENTED_EDGE ( 'NONE', *, *, #1721, .T. ) ;
#15778=CARTESIAN_POINT ( 'NONE',  ( 1.845714884748260509, 0.000000000000000000, -2.498788568296995916 ) ) ;
#15789=CIRCLE ( 'NONE', #8760, 0.4062499999999995004 ) ;
#15790=ORIENTED_EDGE ( 'NONE', *, *, #3957, .T. ) ;
#15828=ORIENTED_EDGE ( 'NONE', *, *, #8255, .F. ) ;
#15830=LINE ( 'NONE', #3144, #10159 ) ;
#15831=LINE ( 'NONE', #23250, #1657 ) ;
#15846=CARTESIAN_POINT ( 'NONE',  ( 1.222470958122163998, 2.978485840173427324, -0.8773620042323713175 ) ) ;
#15859=LINE ( 'NONE', #3053, #22469 ) ;
#15863=DIRECTION ( 'NONE',  ( 0.000000000000000000, 0.000000000000000000, -1.000000000000000000 ) ) ;
#15878=CARTESIAN_POINT ( 'NONE',  ( 0.000000000000000000, 0.000000000000000000, 0.000000000000000000 ) ) ;
#15882=CARTESIAN_POINT ( 'NONE',  ( 0.2703601470917495475, 2.740000000000000213, 0.1560925037015647998 ) ) ;
#15883=ADVANCED_FACE ( 'NONE', ( #2901, #23490, #3145 ), #4847, .T. ) ;
#15894=CARTESIAN_POINT ( 'NONE',  ( 2.296137995767620676, 2.978485840173427324, -2.088288568297006265 ) ) ;
#15914=CARTESIAN_POINT ( 'NONE',  ( 0.5997114317030027841, 2.978485840173427324, -1.206013144887902788 ) ) ;
#15917=EDGE_LOOP ( 'NONE', ( #8308, #16154, #13499, #22743 ) ) ;
#15927=EDGE_CURVE ( 'NONE', #14781, #1954, #19955, .T. ) ;
#15932=AXIS2_PLACEMENT_3D ( 'NONE', #9968, #5931, #7648 ) ;
#15954=DIRECTION ( 'NONE',  ( 0.000000000000000000, 0.000000000000000000, 1.000000000000000000 ) ) ;
#15958=ORIENTED_EDGE ( 'NONE', *, *, #13653, .F. ) ;
#15962=EDGE_CURVE ( 'NONE', #19216, #8072, #15831, .T. ) ;
#15978=DIRECTION ( 'NONE',  ( -0.8660254037844434816, -0.000000000000000000, -0.4999999999999916178 ) ) ;
#15981=EDGE_CURVE ( 'NONE', #6154, #14487, #5085, .T. ) ;
#15992=( BOUNDED_SURFACE ( )  B_SPLINE_SURFACE ( 3, 1, ( 
 ( #6040, #13507 ),
 ( #2991, #19687 ),
 ( #21762, #6762 ),
 ( #23329, #1282 ) ),
 .UNSPECIFIED., .F., .F., .F. ) 
 B_SPLINE_SURFACE_WITH_KNOTS ( ( 4, 4 ),
 ( 2, 2 ),
 ( 0.000000000000000000, 1.000000000000000000 ),
 ( 0.000000000000000000, 1.000000000000000000 ),
 .UNSPECIFIED. ) 
 GEOMETRIC_REPRESENTATION_ITEM ( )  RATIONAL_B_SPLINE_SURFACE ( (
 ( 1.000000000000000000, 1.000000000000000000),
 ( 0.3333333333333338144, 0.3333333333333338144),
 ( 0.3333333333333338144, 0.3333333333333338144),
 ( 1.000000000000000000, 1.000000000000000000) ) ) 
 REPRESENTATION_ITEM ( '' )  SURFACE ( )  );
#15996=ORIENTED_EDGE ( 'NONE', *, *, #9220, .F. ) ;
#16001=CARTESIAN_POINT ( 'NONE',  ( 2.040570600599760365, 0.000000000000000000, -2.386288568296997870 ) ) ;
#16017=LINE ( 'NONE', #6622, #14312 ) ;
#16024=CYLINDRICAL_SURFACE ( 'NONE', #12080, 0.1874999999999998335 ) ;
#16027=VERTEX_POINT ( 'NONE', #17783 ) ;
#16032=EDGE_CURVE ( 'NONE', #16274, #10685, #11318, .T. ) ;
#16039=CARTESIAN_POINT ( 'NONE',  ( 2.911000000000000032, 2.740000000000000213, 0.000000000000000000 ) ) ;
#16040=ORIENTED_EDGE ( 'NONE', *, *, #22827, .T. ) ;
#16072=DIRECTION ( 'NONE',  ( -0.4999999999999918954, -0.000000000000000000, -0.8660254037844432595 ) ) ;
#16087=DIRECTION ( 'NONE',  ( -0.1969820554421523873, -0.5836931634044232320, 0.7877184527664194968 ) ) ;
#16101=FACE_OUTER_BOUND ( 'NONE', #657, .T. ) ;
#16106=EDGE_LOOP ( 'NONE', ( #23823, #20048, #15828, #19072, #6981, #20969 ) ) ;
#16131=EDGE_LOOP ( 'NONE', ( #4194, #18673, #3370, #12921 ) ) ;
#16144=ADVANCED_FACE ( 'NONE', ( #14979 ), #19178, .F. ) ;
#16148=ADVANCED_FACE ( 'NONE', ( #11075 ), #11013, .F. ) ;
#16154=ORIENTED_EDGE ( 'NONE', *, *, #17169, .T. ) ;
#16172=EDGE_CURVE ( 'NONE', #11997, #22384, #20337, .T. ) ;
#16179=VECTOR ( 'NONE', #4631, 39.37007874015748854 ) ;
#16183=EDGE_CURVE ( 'NONE', #12247, #10339, #5577, .T. ) ;
#16201=DIRECTION ( 'NONE',  ( -0.7071067811865435759, -8.268739551449322488E-15, -0.7071067811865513475 ) ) ;
#16202=CARTESIAN_POINT ( 'NONE',  ( 1.787800077107233543, 2.476536290232589810, -1.974119177195009511 ) ) ;
#16206=CARTESIAN_POINT ( 'NONE',  ( 0.6781417736264208074, 2.740000000000000213, 0.3915253355519352496 ) ) ;
#16208=ORIENTED_EDGE ( 'NONE', *, *, #2869, .F. ) ;
#16243=EDGE_CURVE ( 'NONE', #23449, #397, #15336, .T. ) ;
#16249=ORIENTED_EDGE ( 'NONE', *, *, #18910, .F. ) ;
#16252=ORIENTED_EDGE ( 'NONE', *, *, #22697, .F. ) ;
#16274=VERTEX_POINT ( 'NONE', #17165 ) ;
#16275=AXIS2_PLACEMENT_3D ( 'NONE', #14953, #7622, #18602 ) ;
#16288=CARTESIAN_POINT ( 'NONE',  ( 0.4872114317030045716, 2.978485840173427324, -1.400868860739402422 ) ) ;
#16291=EDGE_CURVE ( 'NONE', #12271, #23979, #19107, .T. ) ;
#16314=EDGE_LOOP ( 'NONE', ( #11180, #19496, #21837, #7781 ) ) ;
#16324=DIRECTION ( 'NONE',  ( -0.000000000000000000, -1.000000000000000000, -0.000000000000000000 ) ) ;
#16327=CONICAL_SURFACE ( 'NONE', #8923, 0.4625000000000000777, 0.7853981633974498333 ) ;
#16334=EDGE_CURVE ( 'NONE', #8315, #20541, #13639, .T. ) ;
#16345=LINE ( 'NONE', #23876, #21 ) ;
#16375=ORIENTED_EDGE ( 'NONE', *, *, #3957, .F. ) ;
#16378=DIRECTION ( 'NONE',  ( -1.000000000000000000, 0.000000000000000000, 0.000000000000000000 ) ) ;
#16382=LINE ( 'NONE', #21976, #21942 ) ;
#16386=AXIS2_PLACEMENT_3D ( 'NONE', #5512, #10646, #3317 ) ;
#16404=CARTESIAN_POINT ( 'NONE',  ( 0.05000000000000028727, 2.740000000000000213, 0.000000000000000000 ) ) ;
#16414=EDGE_LOOP ( 'NONE', ( #19878, #10766, #5832, #14244, #12116 ) ) ;
#16419=CARTESIAN_POINT ( 'NONE',  ( 0.5755194329394802688, 2.762520450461519061, -0.7459121653754773318 ) ) ;
#16422=VECTOR ( 'NONE', #16996, 39.37007874015748143 ) ;
#16425=ORIENTED_EDGE ( 'NONE', *, *, #1177, .T. ) ;
#16427=VERTEX_POINT ( 'NONE', #17037 ) ;
#16428=ADVANCED_FACE ( 'NONE', ( #22649 ), #5937, .F. ) ;
#16453=VECTOR ( 'NONE', #14342, 39.37007874015748143 ) ;
#16470=CARTESIAN_POINT ( 'NONE',  ( 0.000000000000000000, 0.05000000000000028727, -2.194053356329904947 ) ) ;
#16478=EDGE_CURVE ( 'NONE', #8144, #22410, #19950, .T. ) ;
#16480=EDGE_CURVE ( 'NONE', #15406, #6253, #21531, .T. ) ;
#16486=ADVANCED_FACE ( 'NONE', ( #10332 ), #5947, .F. ) ;
#16508=CARTESIAN_POINT ( 'NONE',  ( 0.4450000000000002842, 0.000000000000000000, -2.540999999999999925 ) ) ;
#16517=VERTEX_POINT ( 'NONE', #23226 ) ;
#16518=ORIENTED_EDGE ( 'NONE', *, *, #6308, .T. ) ;
#16523=VERTEX_POINT ( 'NONE', #21775 ) ;
#16528=DIRECTION ( 'NONE',  ( 0.7071067811865435759, 0.7071067811865514585, 0.000000000000000000 ) ) ;
#16546=ORIENTED_EDGE ( 'NONE', *, *, #16243, .T. ) ;
#16562=CARTESIAN_POINT ( 'NONE',  ( 2.986000000000000210, 2.740000000000000213, -0.07500000000000014988 ) ) ;
#16563=CARTESIAN_POINT ( 'NONE',  ( 1.938418520877619899, 2.405295409249399441, -1.890758069268034136 ) ) ;
#16575=CARTESIAN_POINT ( 'NONE',  ( 1.573500000000000343, 0.000000000000000000, -0.3524999999999999800 ) ) ;
#16579=CARTESIAN_POINT ( 'NONE',  ( 1.573500000000000343, 0.5250000000000000222, -0.3524999999999999800 ) ) ;
#16587=ORIENTED_EDGE ( 'NONE', *, *, #13344, .F. ) ;
#16621=CARTESIAN_POINT ( 'NONE',  ( 0.9244709581221690620, 2.291712385858714285, -1.333428253224823168 ) ) ;
#16640=CARTESIAN_POINT ( 'NONE',  ( 0.05000000000000028727, 0.000000000000000000, -0.6280533563299045552 ) ) ;
#16645=CIRCLE ( 'NONE', #5742, 0.1874999999999998335 ) ;
#16657=CARTESIAN_POINT ( 'NONE',  ( 0.3949999999999999623, 2.978485840173427324, -0.04999999999999915623 ) ) ;
#16661=VECTOR ( 'NONE', #15954, 39.37007874015748143 ) ;
#16670=CARTESIAN_POINT ( 'NONE',  ( 0.7847114317029997288, 2.291712385858714729, -0.8254988538245822127 ) ) ;
#16674=EDGE_CURVE ( 'NONE', #12233, #15698, #3727, .T. ) ;
#16723=VECTOR ( 'NONE', #4922, 39.37007874015748143 ) ;
#16727=PLANE ( 'NONE',  #11656 ) ;
#16735=CARTESIAN_POINT ( 'NONE',  ( 0.6033333333333333881, 2.873333333333333517, -2.382666666666667155 ) ) ;
#16738=CARTESIAN_POINT ( 'NONE',  ( 0.9287197593527887207, 2.340128234365810300, -1.330304951501487754 ) ) ;
#16754=ORIENTED_EDGE ( 'NONE', *, *, #16674, .F. ) ;
#16757=VECTOR ( 'NONE', #21548, 39.37007874015748143 ) ;
#16759=DIRECTION ( 'NONE',  ( -1.000000000000000000, 0.000000000000000000, 4.440892098500625176E-16 ) ) ;
#16769=DIRECTION ( 'NONE',  ( 0.2610779533529330454, 0.003182690398834837290, 0.9653124741527318031 ) ) ;
#16782=VECTOR ( 'NONE', #13048, 39.37007874015748143 ) ;
#16793=DIRECTION ( 'NONE',  ( 0.000000000000000000, 0.000000000000000000, -1.000000000000000000 ) ) ;
#16807=CARTESIAN_POINT ( 'NONE',  ( 1.655695048498512678, 2.340128234365810744, -2.057280240647211489 ) ) ;
#16816=EDGE_CURVE ( 'NONE', #10130, #23979, #20786, .T. ) ;
#16828=CARTESIAN_POINT ( 'NONE',  ( 0.7919466436700954848, 2.740039370078740433, -2.986000000000000210 ) ) ;
#16847=FACE_OUTER_BOUND ( 'NONE', #18934, .T. ) ;
#16855=VECTOR ( 'NONE', #17664, 39.37007874015748143 ) ;
#16857=EDGE_CURVE ( 'NONE', #10945, #20425, #15072, .T. ) ;
#16878=LINE ( 'NONE', #11162, #3506 ) ;
#16892=EDGE_CURVE ( 'NONE', #12518, #14569, #15426, .T. ) ;
#16899=VERTEX_POINT ( 'NONE', #5908 ) ;
#16901=VECTOR ( 'NONE', #13894, 39.37007874015748854 ) ;
#16902=DIRECTION ( 'NONE',  ( 0.000000000000000000, -1.000000000000000000, -0.000000000000000000 ) ) ;
#16916=DIRECTION ( 'NONE',  ( 0.08715574274765830465, -0.9961946980917454342, -3.870492493070289564E-17 ) ) ;
#16920=VECTOR ( 'NONE', #4656, 39.37007874015748143 ) ;
#16932=CARTESIAN_POINT ( 'NONE',  ( 1.645216030923674522, 2.291712385858714729, -2.498788568296995916 ) ) ;
#16933=DIRECTION ( 'NONE',  ( 0.4999999999999916733, -0.000000000000000000, 0.8660254037844432595 ) ) ;
#16939=LINE ( 'NONE', #22549, #15220 ) ;
#16946=EDGE_CURVE ( 'NONE', #22384, #20123, #19924, .T. ) ;
#16947=PLANE ( 'NONE',  #4594 ) ;
#16971=LINE ( 'NONE', #10270, #5462 ) ;
#16978=EDGE_CURVE ( 'NONE', #16899, #4071, #6626, .T. ) ;
#16986=CARTESIAN_POINT ( 'NONE',  ( 0.3950000000000000178, 0.05000000000000028727, -1.966000000000000192 ) ) ;
#16996=DIRECTION ( 'NONE',  ( -0.000000000000000000, -1.000000000000000000, -0.000000000000000000 ) ) ;
#17004=EDGE_LOOP ( 'NONE', ( #17869, #2595, #22533, #15194, #8618, #20824 ) ) ;
#17019=VECTOR ( 'NONE', #1847, 39.37007874015748854 ) ;
#17020=EDGE_LOOP ( 'NONE', ( #9676, #4566, #16249, #15665, #14006 ) ) ;
#17037=CARTESIAN_POINT ( 'NONE',  ( 0.5800849365154925330, 2.740000000000000213, -0.6888427490622308635 ) ) ;
#17040=VECTOR ( 'NONE', #14367, 39.37007874015748143 ) ;
#17045=PLANE ( 'NONE',  #15557 ) ;
#17048=EDGE_CURVE ( 'NONE', #14200, #15698, #19674, .T. ) ;
#17058=DIRECTION ( 'NONE',  ( 1.707404996040164512E-16, 0.000000000000000000, -1.000000000000000000 ) ) ;
#17062=LINE ( 'NONE', #9508, #3652 ) ;
#17070=EDGE_LOOP ( 'NONE', ( #9168, #18101 ) ) ;
#17072=VECTOR ( 'NONE', #14821, 39.37007874015748143 ) ;
#17078=ADVANCED_FACE ( 'NONE', ( #10787 ), #13463, .T. ) ;
#17095=DIRECTION ( 'NONE',  ( -1.000000000000000000, 0.000000000000000000, 0.000000000000000000 ) ) ;
#17099=DIRECTION ( 'NONE',  ( 0.8660254037844434816, 0.000000000000000000, -0.4999999999999914513 ) ) ;
#17106=CARTESIAN_POINT ( 'NONE',  ( 0.03174294256098300626, 2.685901063997346405, -0.8524985337548631747 ) ) ;
#17107=VERTEX_POINT ( 'NONE', #7944 ) ;
#17114=EDGE_CURVE ( 'NONE', #11818, #9048, #6239, .T. ) ;
#17116=VERTEX_POINT ( 'NONE', #15517 ) ;
#17119=CARTESIAN_POINT ( 'NONE',  ( 0.7948333950160438865, 2.675000000000000711, -3.001000000000001666 ) ) ;
#17133=CARTESIAN_POINT ( 'NONE',  ( 0.8977114317029943891, 2.291712385858714729, -0.6297771125693037986 ) ) ;
#17137=LINE ( 'NONE', #5674, #3816 ) ;
#17146=VERTEX_POINT ( 'NONE', #512 ) ;
#17148=PLANE ( 'NONE',  #11478 ) ;
#17163=EDGE_CURVE ( 'NONE', #7263, #23447, #22828, .T. ) ;
#17165=CARTESIAN_POINT ( 'NONE',  ( 1.457716030923678074, 2.291712385858714729, -2.174029041877829194 ) ) ;
#17168=AXIS2_PLACEMENT_3D ( 'NONE', #22094, #16378, #14306 ) ;
#17169=EDGE_CURVE ( 'NONE', #15406, #2181, #22310, .T. ) ;
#17174=ORIENTED_EDGE ( 'NONE', *, *, #2660, .T. ) ;
#17186=LINE ( 'NONE', #16828, #3913 ) ;
#17206=LINE ( 'NONE', #3794, #9194 ) ;
#17224=ADVANCED_FACE ( 'NONE', ( #22706 ), #636, .F. ) ;
#17269=CARTESIAN_POINT ( 'NONE',  ( 1.617249732617304092, 2.740000000000000213, -2.801158705420349726 ) ) ;
#17287=PLANE ( 'NONE',  #14735 ) ;
#17303=ORIENTED_EDGE ( 'NONE', *, *, #23714, .F. ) ;
#17310=DIRECTION ( 'NONE',  ( -0.8651979924482607887, 0.04370253788966922681, 0.4995222938423281578 ) ) ;
#17312=LINE ( 'NONE', #19380, #7147 ) ;
#17313=ORIENTED_EDGE ( 'NONE', *, *, #906, .F. ) ;
#17322=PLANE ( 'NONE',  #1742 ) ;
#17324=EDGE_CURVE ( 'NONE', #16523, #1066, #2946, .T. ) ;
#17345=LINE ( 'NONE', #11506, #1546 ) ;
#17347=CARTESIAN_POINT ( 'NONE',  ( 0.000000000000000000, 2.740000000000000213, -0.05000000000000028727 ) ) ;
#17354=VECTOR ( 'NONE', #1042, 39.37007874015748143 ) ;
#17357=ORIENTED_EDGE ( 'NONE', *, *, #16892, .T. ) ;
#17378=ORIENTED_EDGE ( 'NONE', *, *, #22827, .F. ) ;
#17384=DIRECTION ( 'NONE',  ( -1.000000000000000000, 0.000000000000000000, 0.000000000000000000 ) ) ;
#17387=AXIS2_PLACEMENT_3D ( 'NONE', #15846, #1779, #17796 ) ;
#17417=AXIS2_PLACEMENT_3D ( 'NONE', #1195, #6800, #10230 ) ;
#17420=DIRECTION ( 'NONE',  ( 0.08715574274765830465, -0.9961946980917454342, -3.870492493070289564E-17 ) ) ;
#17438=VECTOR ( 'NONE', #15757, 39.37007874015748143 ) ;
#17451=FACE_OUTER_BOUND ( 'NONE', #16414, .T. ) ;
#17461=EDGE_CURVE ( 'NONE', #5470, #8054, #5125, .T. ) ;
#17475=EDGE_LOOP ( 'NONE', ( #19959, #23541, #21307, #337 ) ) ;
#17485=DIRECTION ( 'NONE',  ( 0.8660254037844438146, 0.000000000000000000, 0.4999999999999910627 ) ) ;
#17489=ADVANCED_FACE ( 'NONE', ( #3182 ), #1830, .F. ) ;
#17502=VECTOR ( 'NONE', #2182, 39.37007874015748854 ) ;
#17506=PLANE ( 'NONE',  #10267 ) ;
#17510=ORIENTED_EDGE ( 'NONE', *, *, #17528, .T. ) ;
#17525=ORIENTED_EDGE ( 'NONE', *, *, #23584, .T. ) ;
#17528=EDGE_CURVE ( 'NONE', #7579, #21713, #22075, .T. ) ;
#17537=VECTOR ( 'NONE', #11462, 39.37007874015748854 ) ;
#17539=CARTESIAN_POINT ( 'NONE',  ( 0.3950000000000000178, 2.665000000000000036, -0.2605837454876624437 ) ) ;
#17543=EDGE_LOOP ( 'NONE', ( #9287, #1276, #4441, #14672 ) ) ;
#17545=DIRECTION ( 'NONE',  ( -0.000000000000000000, -1.000000000000000000, -0.000000000000000000 ) ) ;
#17566=DIRECTION ( 'NONE',  ( -0.7745966692414836263, -0.4472135954999552077, -0.4472135954999600926 ) ) ;
#17567=CARTESIAN_POINT ( 'NONE',  ( 0.03174294256098305483, 2.685901063997346405, -0.8524985337548631747 ) ) ;
#17575=CARTESIAN_POINT ( 'NONE',  ( 0.3950000000000000178, 2.665000000000000036, -2.591000000000000192 ) ) ;
#17579=VECTOR ( 'NONE', #4808, 39.37007874015748854 ) ;
#17633=AXIS2_PLACEMENT_3D ( 'NONE', #19580, #14103, #1174 ) ;
#17646=ORIENTED_EDGE ( 'NONE', *, *, #8703, .T. ) ;
#17661=ORIENTED_EDGE ( 'NONE', *, *, #14495, .F. ) ;
#17664=DIRECTION ( 'NONE',  ( 0.4999999999999760192, 0.000000000000000000, -0.8660254037844524744 ) ) ;
#17670=PLANE ( 'NONE',  #3828 ) ;
#17674=ORIENTED_EDGE ( 'NONE', *, *, #20656, .F. ) ;
#17684=CARTESIAN_POINT ( 'NONE',  ( 0.3247595264191666109, 2.291712385858714285, -0.9871846966950065250 ) ) ;
#17706=AXIS2_PLACEMENT_3D ( 'NONE', #4805, #2631, #19333 ) ;
#17721=AXIS2_PLACEMENT_3D ( 'NONE', #13000, #20771, #4060 ) ;
#17730=LINE ( 'NONE', #21505, #17910 ) ;
#17736=VECTOR ( 'NONE', #3494, 39.37007874015748143 ) ;
#17738=ORIENTED_EDGE ( 'NONE', *, *, #21969, .T. ) ;
#17742=DIRECTION ( 'NONE',  ( -0.08715574274765827689, 0.9961946980917454342, 0.000000000000000000 ) ) ;
#17750=EDGE_LOOP ( 'NONE', ( #21072, #14520, #18098, #5343, #19981, #9560, #22470, #21763, #15764, #2956, #7999, #5560, #7659, #3972, #8820, #1410 ) ) ;
#17768=CIRCLE ( 'NONE', #20105, 0.1874999999999998335 ) ;
#17780=ORIENTED_EDGE ( 'NONE', *, *, #5440, .F. ) ;
#17783=CARTESIAN_POINT ( 'NONE',  ( 0.3450849365154919912, 2.740000000000000213, -1.095874688840917210 ) ) ;
#17796=DIRECTION ( 'NONE',  ( -0.4999999999999916733, 0.000000000000000000, -0.8660254037844433705 ) ) ;
#17798=ADVANCED_FACE ( 'NONE', ( #2442 ), #9885, .F. ) ;
#17806=DIRECTION ( 'NONE',  ( 0.4985709748471496283, 0.07555085810113111588, 0.8635502596144277732 ) ) ;
#17813=CARTESIAN_POINT ( 'NONE',  ( 0.000000000000000000, 0.04999999999999919092, 0.000000000000000000 ) ) ;
#17815=EDGE_LOOP ( 'NONE', ( #17948, #7130, #4776, #18880, #4298 ) ) ;
#17816=CARTESIAN_POINT ( 'NONE',  ( 0.000000000000000000, 2.689999999999999947, 0.000000000000000000 ) ) ;
#17823=EDGE_LOOP ( 'NONE', ( #6128, #12851, #17378, #2898 ) ) ;
#17827=ADVANCED_FACE ( 'NONE', ( #15607 ), #9085, .F. ) ;
#17834=EDGE_CURVE ( 'NONE', #11818, #16027, #17312, .T. ) ;
#17835=ORIENTED_EDGE ( 'NONE', *, *, #13344, .T. ) ;
#17838=FACE_OUTER_BOUND ( 'NONE', #847, .T. ) ;
#17852=ORIENTED_EDGE ( 'NONE', *, *, #6757, .T. ) ;
#17857=CARTESIAN_POINT ( 'NONE',  ( 2.936000000000000387, 2.664999999999999591, -2.591000000000000636 ) ) ;
#17869=ORIENTED_EDGE ( 'NONE', *, *, #9220, .T. ) ;
#17872=CARTESIAN_POINT ( 'NONE',  ( 0.4450000000000002842, 0.000000000000000000, -2.591000000000000192 ) ) ;
#17887=DIMENSIONAL_EXPONENTS ( 1.000000000000000000, 0.000000000000000000, 0.000000000000000000, 0.000000000000000000, 0.000000000000000000, 0.000000000000000000, 0.000000000000000000 ) ;
#17907=FACE_OUTER_BOUND ( 'NONE', #77, .T. ) ;
#17910=VECTOR ( 'NONE', #10545, 39.37007874015748854 ) ;
#17914=CARTESIAN_POINT ( 'NONE',  ( 2.586000000000000298, 0.000000000000000000, -2.591000000000000636 ) ) ;
#17916=CARTESIAN_POINT ( 'NONE',  ( 0.03174294256098304789, 2.685901063997346405, -0.8524985337548631747 ) ) ;
#17932=EDGE_CURVE ( 'NONE', #18090, #18008, #6568, .T. ) ;
#17947=AXIS2_PLACEMENT_3D ( 'NONE', #13662, #4367, #11954 ) ;
#17948=ORIENTED_EDGE ( 'NONE', *, *, #23175, .F. ) ;
#17949=CARTESIAN_POINT ( 'NONE',  ( 0.3950000000000000733, 0.04999999999999919092, -0.2605837454876624437 ) ) ;
#17970=CARTESIAN_POINT ( 'NONE',  ( 1.573500000000000343, 0.02500000000000021302, -0.3524999999999999800 ) ) ;
#17976=DIRECTION ( 'NONE',  ( 0.4999999999999912292, 0.000000000000000000, -0.8660254037844437036 ) ) ;
#17987=ORIENTED_EDGE ( 'NONE', *, *, #10068, .T. ) ;
#17990=CARTESIAN_POINT ( 'NONE',  ( 2.973500000000002252, 2.702500000000001013, -2.553499999999999215 ) ) ;
#18008=VERTEX_POINT ( 'NONE', #740 ) ;
#18011=DIRECTION ( 'NONE',  ( -0.3535533905932763399, -0.7071067811865430208, 0.6123724356957982451 ) ) ;
#18027=CARTESIAN_POINT ( 'NONE',  ( 1.973001146175422216, 2.291712385858714729, -1.876529041877834203 ) ) ;
#18030=DIRECTION ( 'NONE',  ( -0.8660254037844434816, -0.000000000000000000, -0.4999999999999914513 ) ) ;
#18054=CARTESIAN_POINT ( 'NONE',  ( 2.827183371398320766, 0.9578965207785177238, -3.893896520778517889 ) ) ;
#18081=CARTESIAN_POINT ( 'NONE',  ( 0.3950000000000000178, 2.665000000000000036, -1.966000000000000192 ) ) ;
#18090=VERTEX_POINT ( 'NONE', #21347 ) ;
#18098=ORIENTED_EDGE ( 'NONE', *, *, #9458, .T. ) ;
#18101=ORIENTED_EDGE ( 'NONE', *, *, #20471, .T. ) ;
#18104=EDGE_CURVE ( 'NONE', #16027, #16427, #6465, .T. ) ;
#18126=CIRCLE ( 'NONE', #1756, 0.4062499999999997780 ) ;
#18132=EDGE_CURVE ( 'NONE', #18537, #23057, #7929, .T. ) ;
#18166=CIRCLE ( 'NONE', #20501, 0.1850000000000000533 ) ;
#18183=CARTESIAN_POINT ( 'NONE',  ( 0.7919466436700954848, 2.665000000000000036, -2.986000000000000210 ) ) ;
#18193=ORIENTED_EDGE ( 'NONE', *, *, #13057, .T. ) ;
#18195=DIRECTION ( 'NONE',  ( 0.7071067811865474617, -0.7071067811865474617, -0.000000000000000000 ) ) ;
#18196=ORIENTED_EDGE ( 'NONE', *, *, #21533, .F. ) ;
#18198=ORIENTED_EDGE ( 'NONE', *, *, #1140, .T. ) ;
#18206=CARTESIAN_POINT ( 'NONE',  ( 0.3247595264191642794, 2.291712385858714729, -0.9871846966950100777 ) ) ;
#18221=VERTEX_POINT ( 'NONE', #11608 ) ;
#18223=CIRCLE ( 'NONE', #4188, 0.4625000000000000777 ) ;
#18229=ORIENTED_EDGE ( 'NONE', *, *, #17048, .F. ) ;
#18235=ORIENTED_EDGE ( 'NONE', *, *, #4739, .F. ) ;
#18247=DIRECTION ( 'NONE',  ( 0.5773502691896283956, -0.5773502691896220673, -0.5773502691896265082 ) ) ;
#18252=VECTOR ( 'NONE', #4276, 39.37007874015748854 ) ;
#18266=DIRECTION ( 'NONE',  ( 0.000000000000000000, -1.000000000000000000, 0.000000000000000000 ) ) ;
#18271=EDGE_CURVE ( 'NONE', #21713, #21079, #3376, .T. ) ;
#18279=FACE_OUTER_BOUND ( 'NONE', #18849, .T. ) ;
#18307=AXIS2_PLACEMENT_3D ( 'NONE', #4869, #17806, #12451 ) ;
#18315=CARTESIAN_POINT ( 'NONE',  ( 0.000000000000000000, 2.740000000000000213, 0.000000000000000000 ) ) ;
#18318=PLANE ( 'NONE',  #6097 ) ;
#18323=VECTOR ( 'NONE', #18504, 39.37007874015748854 ) ;
#18325=CARTESIAN_POINT ( 'NONE',  ( 1.036069691232456069, 2.476534978792082509, -1.156303459062617556 ) ) ;
#18331=ADVANCED_FACE ( 'NONE', ( #20449 ), #22029, .T. ) ;
#18332=PLANE ( 'NONE',  #13830 ) ;
#18348=CARTESIAN_POINT ( 'NONE',  ( 0.3950000000000000178, 2.740039370078740433, -1.966000000000000192 ) ) ;
#18351=DIRECTION ( 'NONE',  ( 0.000000000000000000, 0.000000000000000000, -1.000000000000000000 ) ) ;
#18365=EDGE_CURVE ( 'NONE', #9581, #8250, #1909, .T. ) ;
#18368=DIRECTION ( 'NONE',  ( -0.000000000000000000, -1.000000000000000000, -0.000000000000000000 ) ) ;
#18379=DIRECTION ( 'NONE',  ( -0.000000000000000000, -1.000000000000000000, -0.000000000000000000 ) ) ;
#18380=ORIENTED_EDGE ( 'NONE', *, *, #16946, .T. ) ;
#18385=CARTESIAN_POINT ( 'NONE',  ( 1.972470776266619596, 2.315961009048386643, -1.875610414248984004 ) ) ;
#18397=EDGE_CURVE ( 'NONE', #2181, #12390, #18739, .T. ) ;
#18435=ORIENTED_EDGE ( 'NONE', *, *, #4886, .F. ) ;
#18438=FACE_OUTER_BOUND ( 'NONE', #6970, .T. ) ;
#18442=CARTESIAN_POINT ( 'NONE',  ( 0.05000000000000028727, 0.000000000000000000, -2.194053356329904947 ) ) ;
#18454=VECTOR ( 'NONE', #1107, 39.37007874015748143 ) ;
#18499=CARTESIAN_POINT ( 'NONE',  ( 0.5997114317030027841, 0.000000000000000000, -0.9454293994002404000 ) ) ;
#18504=DIRECTION ( 'NONE',  ( 0.5000000000000037748, 0.000000000000000000, 0.8660254037844362651 ) ) ;
#18505=DIRECTION ( 'NONE',  ( 0.000000000000000000, 0.000000000000000000, 1.000000000000000000 ) ) ;
#18515=DIRECTION ( 'NONE',  ( -1.000000000000000000, 0.000000000000000000, 6.148297094540788948E-16 ) ) ;
#18519=CARTESIAN_POINT ( 'NONE',  ( 0.6107956263425956545, 2.685901063997346405, -1.186814756611144883 ) ) ;
#18521=SHAPE_REPRESENTATION ( 'MAS-409-Body', ( #9127 ), #558 ) ;
#18537=VERTEX_POINT ( 'NONE', #15324 ) ;
#18539=FACE_OUTER_BOUND ( 'NONE', #6451, .T. ) ;
#18554=EDGE_LOOP ( 'NONE', ( #12109, #3908, #11066 ) ) ;
#18555=ORIENTED_EDGE ( 'NONE', *, *, #16478, .T. ) ;
#18557=CARTESIAN_POINT ( 'NONE',  ( 2.285240235267019138, 2.686579321989253089, -2.477179094559016193 ) ) ;
#18566=ADVANCED_FACE ( 'NONE', ( #19340 ), #17506, .F. ) ;
#18580=ORIENTED_EDGE ( 'NONE', *, *, #8731, .T. ) ;
#18592=CARTESIAN_POINT ( 'NONE',  ( 0.5129115487115525340, 2.693521551442877193, -0.7037288651031901043 ) ) ;
#18602=DIRECTION ( 'NONE',  ( 0.000000000000000000, -0.000000000000000000, -1.000000000000000000 ) ) ;
#18611=CARTESIAN_POINT ( 'NONE',  ( 2.295391506243690927, 2.740000000000000213, -2.409633369868423358 ) ) ;
#18616=CARTESIAN_POINT ( 'NONE',  ( 2.386814157129576675, 0.000000000000000000, -2.935999999999999943 ) ) ;
#18628=CARTESIAN_POINT ( 'NONE',  ( 1.973001146175422216, 2.291712385858714729, -1.876529041877834203 ) ) ;
#18631=CARTESIAN_POINT ( 'NONE',  ( 0.4199999999999995959, 0.04999999999999921868, -0.02499999999999958505 ) ) ;
#18633=CARTESIAN_POINT ( 'NONE',  ( 2.055580586463031434, 2.740000000000000213, -2.936000000000001720 ) ) ;
#18634=FACE_OUTER_BOUND ( 'NONE', #19905, .T. ) ;
#18636=AXIS2_PLACEMENT_3D ( 'NONE', #21849, #12366, #19783 ) ;
#18651=CARTESIAN_POINT ( 'NONE',  ( 1.573500000000000343, 0.5250000000000000222, -0.1650000000000001465 ) ) ;
#18673=ORIENTED_EDGE ( 'NONE', *, *, #17169, .F. ) ;
#18696=EDGE_CURVE ( 'NONE', #1943, #21079, #23912, .T. ) ;
#18698=EDGE_CURVE ( 'NONE', #22988, #8072, #16382, .T. ) ;
#18699=VERTEX_POINT ( 'NONE', #21859 ) ;
#18704=CARTESIAN_POINT ( 'NONE',  ( 2.345681073014820761, 0.05000000000000028727, -2.986000000000000210 ) ) ;
#18722=LINE ( 'NONE', #2140, #6085 ) ;
#18739=LINE ( 'NONE', #10947, #11427 ) ;
#18750=CARTESIAN_POINT ( 'NONE',  ( 1.728575740896261204, 2.453214835500605595, -2.009490367722004400 ) ) ;
#18753=DIRECTION ( 'NONE',  ( 1.000000000000000000, 0.000000000000000000, 0.000000000000000000 ) ) ;
#18754=CARTESIAN_POINT ( 'NONE',  ( 1.573500000000000343, -3.414809992080329023E-17, -0.9499999999999999556 ) ) ;
#18761=DIRECTION ( 'NONE',  ( -0.8660254037844433705, 0.000000000000000000, 0.4999999999999917843 ) ) ;
#18771=DIRECTION ( 'NONE',  ( -1.000000000000000000, 0.000000000000000000, 0.000000000000000000 ) ) ;
#18783=VECTOR ( 'NONE', #12553, 39.37007874015748143 ) ;
#18800=VECTOR ( 'NONE', #19434, 39.37007874015748143 ) ;
#18801=CARTESIAN_POINT ( 'NONE',  ( 0.8043248696826207356, 2.291712385858714285, -0.5923223533918536843 ) ) ;
#18802=DIRECTION ( 'NONE',  ( 0.000000000000000000, 0.000000000000000000, -1.000000000000000000 ) ) ;
#18804=CARTESIAN_POINT ( 'NONE',  ( 0.9253895857510197054, 2.315961009048385755, -1.333958623133626009 ) ) ;
#18810=ORIENTED_EDGE ( 'NONE', *, *, #2627, .F. ) ;
#18815=CARTESIAN_POINT ( 'NONE',  ( 1.951887815886574673, 2.740000000000000213, -1.126922955930076409 ) ) ;
#18816=VECTOR ( 'NONE', #3496, 39.37007874015748143 ) ;
#18822=ORIENTED_EDGE ( 'NONE', *, *, #3105, .F. ) ;
#18827=VERTEX_POINT ( 'NONE', #20751 ) ;
#18843=EDGE_CURVE ( 'NONE', #17116, #20229, #22698, .T. ) ;
#18849=EDGE_LOOP ( 'NONE', ( #12351, #22005, #6634, #15958 ) ) ;
#18859=APPLICATION_CONTEXT ( 'configuration controlled 3d designs of mechanical parts and assemblies' ) ;
#18875=EDGE_CURVE ( 'NONE', #23057, #1821, #1851, .T. ) ;
#18878=DIRECTION ( 'NONE',  ( 0.000000000000000000, 0.000000000000000000, -1.000000000000000000 ) ) ;
#18880=ORIENTED_EDGE ( 'NONE', *, *, #2767, .F. ) ;
#18899=CARTESIAN_POINT ( 'NONE',  ( 0.4449999999999991740, 2.689999999999999947, 0.000000000000000000 ) ) ;
#18910=EDGE_CURVE ( 'NONE', #21079, #24062, #11864, .T. ) ;
#18919=DIRECTION ( 'NONE',  ( 0.000000000000000000, 0.000000000000000000, 1.000000000000000000 ) ) ;
#18923=VECTOR ( 'NONE', #14661, 39.37007874015748854 ) ;
#18934=EDGE_LOOP ( 'NONE', ( #22610, #2363, #17525, #23114 ) ) ;
#18942=LINE ( 'NONE', #9671, #3489 ) ;
#18972=B_SPLINE_CURVE_WITH_KNOTS ( 'NONE', 3,
 ( #7116, #20156, #24041, #9421, #3812, #5761, #1738, #14917, #18325, #14802, #145, #9298, #23794, #21978, #9177, #16738, #18804, #16621 ),
 .UNSPECIFIED., .F., .F.,
 ( 4, 2, 2, 2, 2, 2, 2, 2, 4 ),
 ( 0.000000000000000000, 0.001843124596548149008, 0.003686249193096298015, 0.005529373789644447673, 0.007372498386192604704, 0.009215622982740761734, 0.01105874757928891963, 0.01290187217583707580, 0.01474499677238523196 ),
 .UNSPECIFIED. ) ;
#18995=LINE ( 'NONE', #5702, #6118 ) ;
#18997=VECTOR ( 'NONE', #22996, 39.37007874015748854 ) ;
#19011=VERTEX_POINT ( 'NONE', #986 ) ;
#19016=CARTESIAN_POINT ( 'NONE',  ( 2.369221741255291391, 0.000000000000000000, -1.763529041877836434 ) ) ;
#19018=ADVANCED_FACE ( 'NONE', ( #23161 ), #15629, .T. ) ;
#19020=CARTESIAN_POINT ( 'NONE',  ( 0.3949999999999999623, 2.665000000000000036, -0.04999999999999915623 ) ) ;
#19029=EDGE_LOOP ( 'NONE', ( #23487, #17174, #3578, #5612, #8186 ) ) ;
#19039=DIRECTION ( 'NONE',  ( -1.000000000000000000, 0.000000000000000000, 0.000000000000000000 ) ) ;
#19058=( LENGTH_UNIT ( ) NAMED_UNIT ( * ) SI_UNIT ( $, .METRE. ) );
#19064=ORIENTED_EDGE ( 'NONE', *, *, #6672, .T. ) ;
#19072=ORIENTED_EDGE ( 'NONE', *, *, #14994, .F. ) ;
#19073=LINE ( 'NONE', #9817, #9244 ) ;
#19107=LINE ( 'NONE', #4107, #14913 ) ;
#19114=DIRECTION ( 'NONE',  ( 0.8660254037844438146, 0.000000000000000000, 0.4999999999999910627 ) ) ;
#19169=EDGE_CURVE ( 'NONE', #22410, #20541, #2500, .T. ) ;
#19175=CARTESIAN_POINT ( 'NONE',  ( 2.557132486540519611, 0.000000000000000000, -2.541000000000000369 ) ) ;
#19178=CONICAL_SURFACE ( 'NONE', #872, 0.4062499999999995004, 0.7853981633974482790 ) ;
#19189=DIRECTION ( 'NONE',  ( 0.000000000000000000, 0.000000000000000000, 1.000000000000000000 ) ) ;
#19202=ORIENTED_EDGE ( 'NONE', *, *, #22981, .T. ) ;
#19216=VERTEX_POINT ( 'NONE', #1349 ) ;
#19243=DIRECTION ( 'NONE',  ( -0.000000000000000000, -1.000000000000000000, -0.000000000000000000 ) ) ;
#19257=VERTEX_POINT ( 'NONE', #16470 ) ;
#19280=CARTESIAN_POINT ( 'NONE',  ( 0.3950000000000000178, 0.04999999999999921868, -0.04999999999999915623 ) ) ;
#19290=ORIENTED_EDGE ( 'NONE', *, *, #11008, .F. ) ;
#19299=LINE ( 'NONE', #11514, #3135 ) ;
#19301=EDGE_CURVE ( 'NONE', #18008, #7579, #12582, .T. ) ;
#19306=VERTEX_POINT ( 'NONE', #6712 ) ;
#19323=LINE ( 'NONE', #2621, #13232 ) ;
#19328=VERTEX_POINT ( 'NONE', #3059 ) ;
#19329=ORIENTED_EDGE ( 'NONE', *, *, #566, .F. ) ;
#19333=DIRECTION ( 'NONE',  ( 0.000000000000000000, 0.000000000000000000, -1.000000000000000000 ) ) ;
#19340=FACE_OUTER_BOUND ( 'NONE', #1253, .T. ) ;
#19355=AXIS2_PLACEMENT_3D ( 'NONE', #6831, #6467, #21349 ) ;
#19357=EDGE_LOOP ( 'NONE', ( #15053, #10529, #4827, #311 ) ) ;
#19364=VECTOR ( 'NONE', #1019, 39.37007874015748854 ) ;
#19365=LINE ( 'NONE', #10228, #16757 ) ;
#19371=EDGE_CURVE ( 'NONE', #12633, #9048, #5842, .T. ) ;
#19379=LINE ( 'NONE', #13902, #20675 ) ;
#19380=CARTESIAN_POINT ( 'NONE',  ( 0.3719562388801891939, 2.800349848324033442, -1.181074844845517058 ) ) ;
#19401=DIRECTION ( 'NONE',  ( 1.000000000000000000, 0.000000000000000000, -0.000000000000000000 ) ) ;
#19410=ORIENTED_EDGE ( 'NONE', *, *, #13083, .T. ) ;
#19421=CARTESIAN_POINT ( 'NONE',  ( 0.9074166975080198982, 2.740000000000000213, -2.936000000000001720 ) ) ;
#19422=VERTEX_POINT ( 'NONE', #18651 ) ;
#19434=DIRECTION ( 'NONE',  ( -0.000000000000000000, 0.9961946980917454342, -0.08715574274765824914 ) ) ;
#19446=EDGE_CURVE ( 'NONE', #16899, #13618, #17062, .T. ) ;
#19481=VECTOR ( 'NONE', #17095, 39.37007874015748143 ) ;
#19496=ORIENTED_EDGE ( 'NONE', *, *, #8284, .T. ) ;
#19497=VERTEX_POINT ( 'NONE', #3779 ) ;
#19498=LINE ( 'NONE', #2681, #24111 ) ;
#19506=LINE ( 'NONE', #972, #6876 ) ;
#19509=CARTESIAN_POINT ( 'NONE',  ( 0.4057955023597048516, 2.693521551442877193, -0.6418853869074238050 ) ) ;
#19520=CARTESIAN_POINT ( 'NONE',  ( 0.4450000000000002842, 0.000000000000000000, -2.540999999999999925 ) ) ;
#19530=ORIENTED_EDGE ( 'NONE', *, *, #19169, .T. ) ;
#19533=PLANE ( 'NONE',  #10694 ) ;
#19534=SHAPE_REPRESENTATION_RELATIONSHIP ( 'NONE' , 'NONE' ,  #18521, #6219 ) ;
#19535=ORIENTED_EDGE ( 'NONE', *, *, #3824, .F. ) ;
#19538=ORIENTED_EDGE ( 'NONE', *, *, #14761, .F. ) ;
#19541=ORIENTED_EDGE ( 'NONE', *, *, #22229, .T. ) ;
#19552=EDGE_CURVE ( 'NONE', #11335, #13239, #4491, .T. ) ;
#19567=DIRECTION ( 'NONE',  ( 0.000000000000000000, 1.000000000000000000, 0.000000000000000000 ) ) ;
#19569=LINE ( 'NONE', #3887, #8163 ) ;
#19580=CARTESIAN_POINT ( 'NONE',  ( 1.573500000000000343, 0.5250000000000000222, -0.3524999999999999800 ) ) ;
#19623=LINE ( 'NONE', #1094, #10005 ) ;
#19637=DIRECTION ( 'NONE',  ( 0.6681584153635196088, -0.6681584153635196088, -0.3273051541876794701 ) ) ;
#19643=EDGE_CURVE ( 'NONE', #17146, #5661, #12431, .T. ) ;
#19653=CARTESIAN_POINT ( 'NONE',  ( 1.573500000000000343, -3.414809992080329023E-17, -0.1400000000000000133 ) ) ;
#19670=LINE ( 'NONE', #18206, #13167 ) ;
#19674=LINE ( 'NONE', #13839, #18800 ) ;
#19681=VECTOR ( 'NONE', #16769, 39.37007874015748854 ) ;
#19686=FACE_OUTER_BOUND ( 'NONE', #1491, .T. ) ;
#19687=CARTESIAN_POINT ( 'NONE',  ( 0.5237631043874195758, 2.661358883302036293, -0.6748402668043530506 ) ) ;
#19689=ORIENTED_EDGE ( 'NONE', *, *, #17114, .T. ) ;
#19694=DIRECTION ( 'NONE',  ( 0.4999999999999913403, 0.000000000000000000, 0.8660254037844434816 ) ) ;
#19695=ORIENTED_EDGE ( 'NONE', *, *, #8725, .T. ) ;
#19697=CARTESIAN_POINT ( 'NONE',  ( 2.122261530980286359, 2.737827333818739106, -2.942657555934166780 ) ) ;
#19698=CARTESIAN_POINT ( 'NONE',  ( 1.109470958122166229, 2.291712385858714285, -1.012998853824579104 ) ) ;
#19704=CARTESIAN_POINT ( 'NONE',  ( 2.296137995767620676, 2.978485840173427324, -2.088288568297006265 ) ) ;
#19710=CARTESIAN_POINT ( 'NONE',  ( 0.4700000000000000844, 2.740000000000000213, 8.024803481388775053E-17 ) ) ;
#19711=ORIENTED_EDGE ( 'NONE', *, *, #199, .T. ) ;
#19721=DIRECTION ( 'NONE',  ( 0.4472135954999557628, 0.4472135954999557628, 0.7745966692414858468 ) ) ;
#19762=EDGE_LOOP ( 'NONE', ( #15790, #22268, #22196, #21019 ) ) ;
#19768=ORIENTED_EDGE ( 'NONE', *, *, #3042, .T. ) ;
#19774=AXIS2_PLACEMENT_3D ( 'NONE', #10994, #23889, #9396 ) ;
#19781=ORIENTED_EDGE ( 'NONE', *, *, #11886, .T. ) ;
#19783=DIRECTION ( 'NONE',  ( 0.000000000000000000, -0.000000000000000000, -1.000000000000000000 ) ) ;
#19787=EDGE_LOOP ( 'NONE', ( #19329, #5751 ) ) ;
#19796=ORIENTED_EDGE ( 'NONE', *, *, #2715, .T. ) ;
#19819=ORIENTED_EDGE ( 'NONE', *, *, #6032, .F. ) ;
#19821=EDGE_LOOP ( 'NONE', ( #15394, #6787, #288, #7183 ) ) ;
#19837=PRODUCT ( 'MAS-409-Body', 'MAS-409-Body', '', ( #10412 ) ) ;
#19855=CARTESIAN_POINT ( 'NONE',  ( 2.319244702705236527, 2.291712385858714285, -2.476240473580833878 ) ) ;
#19878=ORIENTED_EDGE ( 'NONE', *, *, #3372, .F. ) ;
#19892=VERTEX_POINT ( 'NONE', #3505 ) ;
#19895=ADVANCED_FACE ( 'NONE', ( #11073 ), #23850, .F. ) ;
#19905=EDGE_LOOP ( 'NONE', ( #14576, #14754, #16587, #13504 ) ) ;
#19907=CIRCLE ( 'NONE', #14473, 0.4624999999999992450 ) ;
#19909=CARTESIAN_POINT ( 'NONE',  ( 0.4449999999999992295, 0.000000000000000000, -0.04999999999999918399 ) ) ;
#19917=CARTESIAN_POINT ( 'NONE',  ( 0.5997114317030027841, 2.291712385858714729, -1.145928253224826276 ) ) ;
#19918=EDGE_CURVE ( 'NONE', #6853, #19892, #11928, .T. ) ;
#19923=CARTESIAN_POINT ( 'NONE',  ( 1.779986855112097865, 2.978485840173427324, -2.386288568296997870 ) ) ;
#19924=LINE ( 'NONE', #8453, #5166 ) ;
#19935=CARTESIAN_POINT ( 'NONE',  ( 0.4449999999999992295, 0.000000000000000000, -0.04999999999999918399 ) ) ;
#19936=DIRECTION ( 'NONE',  ( -0.8660254037844434816, -0.000000000000000000, -0.4999999999999914513 ) ) ;
#19950=LINE ( 'NONE', #4704, #16453 ) ;
#19955=CIRCLE ( 'NONE', #21510, 0.1850000000000000533 ) ;
#19957=ORIENTED_EDGE ( 'NONE', *, *, #10816, .F. ) ;
#19959=ORIENTED_EDGE ( 'NONE', *, *, #23884, .F. ) ;
#19960=FACE_OUTER_BOUND ( 'NONE', #21167, .T. ) ;
#19981=ORIENTED_EDGE ( 'NONE', *, *, #59, .T. ) ;
#19997=CARTESIAN_POINT ( 'NONE',  ( 1.573500000000000343, 2.683750000000000746, -1.006250000000000533 ) ) ;
#20002=VECTOR ( 'NONE', #10753, 39.37007874015748854 ) ;
#20032=DIRECTION ( 'NONE',  ( -0.4472135954999558738, -0.4472135954999557628, -0.7745966692414858468 ) ) ;
#20034=DIRECTION ( 'NONE',  ( -0.4999999999999760192, 0.000000000000000000, 0.8660254037844524744 ) ) ;
#20048=ORIENTED_EDGE ( 'NONE', *, *, #14238, .T. ) ;
#20052=VERTEX_POINT ( 'NONE', #20821 ) ;
#20054=AXIS2_PLACEMENT_3D ( 'NONE', #6521, #913, #17742 ) ;
#20061=DIRECTION ( 'NONE',  ( 0.08715574274765830465, -0.9961946980917454342, -3.870492493070289564E-17 ) ) ;
#20067=ORIENTED_EDGE ( 'NONE', *, *, #21540, .T. ) ;
#20068=CARTESIAN_POINT ( 'NONE',  ( 2.123323208613025592, 2.690104987760001620, -2.954157130710096002 ) ) ;
#20073=LINE ( 'NONE', #16657, #7308 ) ;
#20082=CLOSED_SHELL ( 'NONE', ( #16148, #509, #16486, #265, #21654, #17827, #11228, #5601, #12375, #21175, #21250, #4008, #10518, #21968, #15883, #5834, #7593, #5894, #19895, #11672, #4823, #9939, #17798, #12588, #6496, #18566, #910, #6030, #23742, #4242, #4544, #4685, #20769, #5305, #18331, #20493, #9379, #3791, #9125, #20925, #15375, #3367, #16144, #6722, #7721, #2602, #8019, #15733, #6782, #1689, #4144, #5703, #10014, #9737, #17224, #4655, #20994, #12310, #16428, #12127, #21529, #19018, #13053, #4890, #21431, #6780, #7695, #10487, #12470, #5889, #10135, #10348, #2162, #17078, #7196, #21236, #8427, #23207, #8321, #23075, #4387, #7400, #22412, #17489, #24117 ) ) ;
#20084=VECTOR ( 'NONE', #4582, 39.37007874015748143 ) ;
#20093=LINE ( 'NONE', #2814, #7417 ) ;
#20104=ORIENTED_EDGE ( 'NONE', *, *, #16183, .T. ) ;
#20105=AXIS2_PLACEMENT_3D ( 'NONE', #10940, #18368, #23384 ) ;
#20123=VERTEX_POINT ( 'NONE', #12053 ) ;
#20136=EDGE_CURVE ( 'NONE', #5797, #18537, #4055, .T. ) ;
#20150=DIRECTION ( 'NONE',  ( 1.000000000000000000, 0.000000000000000000, -6.148297094540788948E-16 ) ) ;
#20156=CARTESIAN_POINT ( 'NONE',  ( 1.110389585751016872, 2.315961009048385755, -1.013529223733381057 ) ) ;
#20174=AXIS2_PLACEMENT_3D ( 'NONE', #18183, #1477, #4650 ) ;
#20181=DIRECTION ( 'NONE',  ( -0.5000000000000037748, 0.000000000000000000, -0.8660254037844362651 ) ) ;
#20184=CARTESIAN_POINT ( 'NONE',  ( 1.573500000000000343, 0.000000000000000000, -1.412500000000000089 ) ) ;
#20207=AXIS2_PLACEMENT_3D ( 'NONE', #4429, #2614, #21264 ) ;
#20208=CARTESIAN_POINT ( 'NONE',  ( 2.346281061938968016, 2.740000000000000213, -2.515999999999999570 ) ) ;
#20214=CARTESIAN_POINT ( 'NONE',  ( 3.882666666666670707, 0.9466666666666798680, -0.9716666666666702312 ) ) ;
#20226=VERTEX_POINT ( 'NONE', #16986 ) ;
#20229=VERTEX_POINT ( 'NONE', #13341 ) ;
#20232=CARTESIAN_POINT ( 'NONE',  ( 0.3950000000000000178, 0.05000000000000028727, -2.540999999999999925 ) ) ;
#20243=CARTESIAN_POINT ( 'NONE',  ( 2.581625566823704254, 0.04999999999999919092, -2.591000000000000636 ) ) ;
#20246=EDGE_LOOP ( 'NONE', ( #8777, #2773, #20104, #3396 ) ) ;
#20263=VECTOR ( 'NONE', #20871, 39.37007874015748854 ) ;
#20267=CARTESIAN_POINT ( 'NONE',  ( 0.4450000000000002842, 0.000000000000000000, -2.540999999999999925 ) ) ;
#20298=LINE ( 'NONE', #22354, #17072 ) ;
#20320=FACE_OUTER_BOUND ( 'NONE', #2654, .T. ) ;
#20337=LINE ( 'NONE', #14865, #23448 ) ;
#20348=AXIS2_PLACEMENT_3D ( 'NONE', #10360, #10236, #6806 ) ;
#20351=EDGE_CURVE ( 'NONE', #23278, #5903, #13817, .T. ) ;
#20361=EDGE_CURVE ( 'NONE', #12518, #6853, #15643, .T. ) ;
#20387=EDGE_LOOP ( 'NONE', ( #435, #23089, #5443, #285 ) ) ;
#20391=DIRECTION ( 'NONE',  ( 1.049727191138617463E-16, -0.5150380749100555988, 0.8571673007021114454 ) ) ;
#20407=VECTOR ( 'NONE', #15863, 39.37007874015748143 ) ;
#20418=DIRECTION ( 'NONE',  ( -0.000000000000000000, -0.9961946980917454342, 0.08715574274765830465 ) ) ;
#20421=CARTESIAN_POINT ( 'NONE',  ( 1.585131139260598010, 2.978485840173427324, -2.498788568296995916 ) ) ;
#20425=VERTEX_POINT ( 'NONE', #19175 ) ;
#20449=FACE_OUTER_BOUND ( 'NONE', #5439, .T. ) ;
#20457=CARTESIAN_POINT ( 'NONE',  ( 1.840071746775174377, 2.291712385858714729, -2.386288568296997425 ) ) ;
#20459=CARTESIAN_POINT ( 'NONE',  ( 1.850761986253052660, 2.471736157945122692, -1.938010564379532674 ) ) ;
#20470=VECTOR ( 'NONE', #20061, 39.37007874015748143 ) ;
#20471=EDGE_CURVE ( 'NONE', #11997, #14781, #5223, .T. ) ;
#20474=DIRECTION ( 'NONE',  ( -0.000000000000000000, -1.000000000000000000, -0.000000000000000000 ) ) ;
#20492=ORIENTED_EDGE ( 'NONE', *, *, #2869, .T. ) ;
#20493=ADVANCED_FACE ( 'NONE', ( #10044 ), #19533, .T. ) ;
#20501=AXIS2_PLACEMENT_3D ( 'NONE', #5101, #12815, #3521 ) ;
#20507=VERTEX_POINT ( 'NONE', #21484 ) ;
#20510=LINE ( 'NONE', #12, #17019 ) ;
#20515=DIRECTION ( 'NONE',  ( -0.5000000000000037748, 0.000000000000000000, -0.8660254037844362651 ) ) ;
#20533=ORIENTED_EDGE ( 'NONE', *, *, #1550, .T. ) ;
#20541=VERTEX_POINT ( 'NONE', #19653 ) ;
#20560=DIRECTION ( 'NONE',  ( -0.6414950336115150531, 0.5424408363369016550, 0.5424408363369075392 ) ) ;
#20615=DIRECTION ( 'NONE',  ( -0.000000000000000000, -1.000000000000000000, -0.000000000000000000 ) ) ;
#20626=LINE ( 'NONE', #9291, #19481 ) ;
#20640=ORIENTED_EDGE ( 'NONE', *, *, #14238, .F. ) ;
#20656=EDGE_CURVE ( 'NONE', #24096, #18008, #7569, .T. ) ;
#20658=CARTESIAN_POINT ( 'NONE',  ( 2.986000000000000210, 0.05000000000000028727, -0.07500000000000014988 ) ) ;
#20675=VECTOR ( 'NONE', #10243, 39.37007874015748143 ) ;
#20686=LINE ( 'NONE', #11428, #6842 ) ;
#20700=FACE_OUTER_BOUND ( 'NONE', #17070, .T. ) ;
#20705=CARTESIAN_POINT ( 'NONE',  ( 0.5097595264191659981, 2.291712385858714729, -0.6667552972947653478 ) ) ;
#20727=ORIENTED_EDGE ( 'NONE', *, *, #13818, .F. ) ;
#20731=VECTOR ( 'NONE', #16916, 39.37007874015748143 ) ;
#20751=CARTESIAN_POINT ( 'NONE',  ( 2.948500000000001009, 2.727500000000000924, -0.03750000000000084516 ) ) ;
#20752=LINE ( 'NONE', #9788, #10140 ) ;
#20769=ADVANCED_FACE ( 'NONE', ( #732 ), #13788, .F. ) ;
#20771=DIRECTION ( 'NONE',  ( 0.000000000000000000, 0.000000000000000000, 1.000000000000000000 ) ) ;
#20786=LINE ( 'NONE', #540, #11030 ) ;
#20792=EDGE_CURVE ( 'NONE', #7614, #22384, #13909, .T. ) ;
#20819=CARTESIAN_POINT ( 'NONE',  ( 2.159030003005114828, 2.291712385858714285, -2.568740473580834127 ) ) ;
#20821=CARTESIAN_POINT ( 'NONE',  ( 2.356802308782948607, 2.740000000000000213, -2.515999999999999570 ) ) ;
#20824=ORIENTED_EDGE ( 'NONE', *, *, #15576, .F. ) ;
#20826=ORIENTED_EDGE ( 'NONE', *, *, #22035, .T. ) ;
#20832=DIRECTION ( 'NONE',  ( -0.000000000000000000, -1.000000000000000000, -0.000000000000000000 ) ) ;
#20841=CARTESIAN_POINT ( 'NONE',  ( -0.1532564258214290931, 2.740000000000000213, -0.2654479161091319872 ) ) ;
#20851=ORIENTED_EDGE ( 'NONE', *, *, #3016, .T. ) ;
#20854=VECTOR ( 'NONE', #3117, 39.37007874015748143 ) ;
#20871=DIRECTION ( 'NONE',  ( -0.4999999999999913403, -0.000000000000000000, -0.8660254037844434816 ) ) ;
#20879=CARTESIAN_POINT ( 'NONE',  ( 2.986000000000000210, 2.740000000000000213, -0.07500000000000014988 ) ) ;
#20884=VECTOR ( 'NONE', #4314, 39.37007874015748854 ) ;
#20900=ORIENTED_EDGE ( 'NONE', *, *, #23604, .F. ) ;
#20925=ADVANCED_FACE ( 'NONE', ( #22411 ), #22171, .T. ) ;
#20944=FACE_OUTER_BOUND ( 'NONE', #7156, .T. ) ;
#20945=ORIENTED_EDGE ( 'NONE', *, *, #6757, .F. ) ;
#20947=VERTEX_POINT ( 'NONE', #11692 ) ;
#20950=AXIS2_PLACEMENT_3D ( 'NONE', #22750, #15442, #11913 ) ;
#20952=ORIENTED_EDGE ( 'NONE', *, *, #10068, .F. ) ;
#20969=ORIENTED_EDGE ( 'NONE', *, *, #15576, .T. ) ;
#20991=VERTEX_POINT ( 'NONE', #14478 ) ;
#20994=ADVANCED_FACE ( 'NONE', ( #19960 ), #3131, .F. ) ;
#21003=VECTOR ( 'NONE', #729, 39.37007874015748143 ) ;
#21011=ORIENTED_EDGE ( 'NONE', *, *, #12041, .F. ) ;
#21019=ORIENTED_EDGE ( 'NONE', *, *, #14994, .T. ) ;
#21021=VECTOR ( 'NONE', #3954, 39.37007874015748143 ) ;
#21022=DIRECTION ( 'NONE',  ( -0.5000000000000037748, 0.000000000000000000, -0.8660254037844362651 ) ) ;
#21025=DIRECTION ( 'NONE',  ( -0.000000000000000000, -0.9961946980917454342, 0.08715574274765830465 ) ) ;
#21031=EDGE_LOOP ( 'NONE', ( #14832, #7629, #5243, #17661 ) ) ;
#21034=VECTOR ( 'NONE', #14159, 39.37007874015748854 ) ;
#21036=VECTOR ( 'NONE', #2937, 39.37007874015748854 ) ;
#21050=ORIENTED_EDGE ( 'NONE', *, *, #12539, .F. ) ;
#21072=ORIENTED_EDGE ( 'NONE', *, *, #18104, .T. ) ;
#21079=VERTEX_POINT ( 'NONE', #7513 ) ;
#21090=VERTEX_POINT ( 'NONE', #18611 ) ;
#21097=EDGE_CURVE ( 'NONE', #17146, #20507, #13146, .T. ) ;
#21103=CARTESIAN_POINT ( 'NONE',  ( 0.3950000000000000178, 0.05000000000000028727, -1.966000000000000192 ) ) ;
#21140=PLANE ( 'NONE',  #20207 ) ;
#21142=VERTEX_POINT ( 'NONE', #16508 ) ;
#21144=CARTESIAN_POINT ( 'NONE',  ( 2.319244702705236083, 2.291712385858714729, -2.476240473580833434 ) ) ;
#21154=ORIENTED_EDGE ( 'NONE', *, *, #22834, .T. ) ;
#21167=EDGE_LOOP ( 'NONE', ( #23003, #13116, #14156, #13824, #19711, #5126 ) ) ;
#21172=CARTESIAN_POINT ( 'NONE',  ( 2.986000000000000210, 2.740000000000000213, -2.541000000000000369 ) ) ;
#21175=ADVANCED_FACE ( 'NONE', ( #10542 ), #18332, .T. ) ;
#21185=PRODUCT_DEFINITION ( 'UNKNOWN', '', #9980, #21425 ) ;
#21232=CARTESIAN_POINT ( 'NONE',  ( 2.986000000000000210, 0.05000000000000028727, -2.591000000000000636 ) ) ;
#21236=ADVANCED_FACE ( 'NONE', ( #15377 ), #22924, .F. ) ;
#21250=ADVANCED_FACE ( 'NONE', ( #15618 ), #17322, .T. ) ;
#21262=CARTESIAN_POINT ( 'NONE',  ( 0.03174294256098306871, 3.006956914082103083, -0.8805872809959580660 ) ) ;
#21264=DIRECTION ( 'NONE',  ( 1.707404996040164512E-16, 0.000000000000000000, -1.000000000000000000 ) ) ;
#21275=ORIENTED_EDGE ( 'NONE', *, *, #10878, .F. ) ;
#21283=LINE ( 'NONE', #13970, #21601 ) ;
#21285=ORIENTED_EDGE ( 'NONE', *, *, #18365, .F. ) ;
#21307=ORIENTED_EDGE ( 'NONE', *, *, #3752, .F. ) ;
#21311=DIRECTION ( 'NONE',  ( -1.000000000000000000, 0.000000000000000000, 0.000000000000000000 ) ) ;
#21315=VECTOR ( 'NONE', #14492, 39.37007874015748143 ) ;
#21337=DIRECTION ( 'NONE',  ( 0.4999999999999909517, -0.000000000000000000, -0.8660254037844438146 ) ) ;
#21347=CARTESIAN_POINT ( 'NONE',  ( 0.000000000000000000, 0.05000000000000028727, -0.6537512679238876023 ) ) ;
#21349=DIRECTION ( 'NONE',  ( -0.5000000000000007772, 0.000000000000000000, -0.8660254037844382635 ) ) ;
#21354=ORIENTED_EDGE ( 'NONE', *, *, #4658, .T. ) ;
#21356=CARTESIAN_POINT ( 'NONE',  ( 0.03174294256098300626, 3.006956914082103083, -0.8805872809959580660 ) ) ;
#21374=CARTESIAN_POINT ( 'NONE',  ( 0.4057955023597048516, 2.693521551442877193, -0.6418853869074238050 ) ) ;
#21390=VECTOR ( 'NONE', #12672, 39.37007874015748854 ) ;
#21423=CARTESIAN_POINT ( 'NONE',  ( -1.562282291722813840E-15, -0.000000000000000000, -2.540999999999999037 ) ) ;
#21425=DESIGN_CONTEXT ( 'detailed design', #22126, 'design' ) ;
#21431=ADVANCED_FACE ( 'NONE', ( #5687 ), #17148, .F. ) ;
#21434=AXIS2_PLACEMENT_3D ( 'NONE', #10532, #12372, #8323 ) ;
#21455=DIRECTION ( 'NONE',  ( 0.5000000000000008882, 0.000000000000000000, 0.8660254037844380415 ) ) ;
#21471=ORIENTED_EDGE ( 'NONE', *, *, #21969, .F. ) ;
#21473=DIRECTION ( 'NONE',  ( 0.000000000000000000, 0.000000000000000000, 1.000000000000000000 ) ) ;
#21484=CARTESIAN_POINT ( 'NONE',  ( 2.055580586463031434, 2.740000000000000213, -2.936000000000001720 ) ) ;
#21491=FACE_OUTER_BOUND ( 'NONE', #9983, .T. ) ;
#21500=EDGE_LOOP ( 'NONE', ( #9554, #7320, #13709 ) ) ;
#21505=CARTESIAN_POINT ( 'NONE',  ( 0.7463359724041158660, 2.506999999999999673, -2.749000000000000554 ) ) ;
#21510=AXIS2_PLACEMENT_3D ( 'NONE', #14491, #21556, #12199 ) ;
#21512=ORIENTED_EDGE ( 'NONE', *, *, #7067, .T. ) ;
#21516=LINE ( 'NONE', #3109, #9276 ) ;
#21529=ADVANCED_FACE ( 'NONE', ( #10197 ), #22977, .T. ) ;
#21531=LINE ( 'NONE', #1420, #3985 ) ;
#21533=EDGE_CURVE ( 'NONE', #20507, #5797, #10441, .T. ) ;
#21540=EDGE_CURVE ( 'NONE', #23820, #24032, #21283, .T. ) ;
#21542=AXIS2_PLACEMENT_3D ( 'NONE', #3615, #11189, #9354 ) ;
#21545=CARTESIAN_POINT ( 'NONE',  ( 0.4450000000000002842, 2.740039370078740433, -2.591000000000000192 ) ) ;
#21548=DIRECTION ( 'NONE',  ( -0.000000000000000000, -1.000000000000000000, -0.000000000000000000 ) ) ;
#21550=CARTESIAN_POINT ( 'NONE',  ( 1.573500000000000343, 0.02500000000000021302, -0.3524999999999999800 ) ) ;
#21556=DIRECTION ( 'NONE',  ( -0.4995222938423280468, -0.04370253788966921987, 0.8651979924482607887 ) ) ;
#21589=CARTESIAN_POINT ( 'NONE',  ( 0.3248054181707789589, 2.594805418170778921, -0.1201945818292202289 ) ) ;
#21601=VECTOR ( 'NONE', #4690, 39.37007874015748143 ) ;
#21609=DIRECTION ( 'NONE',  ( -0.4999999999999912292, 0.000000000000000000, 0.8660254037844437036 ) ) ;
#21611=ORIENTED_EDGE ( 'NONE', *, *, #11219, .T. ) ;
#21642=EDGE_LOOP ( 'NONE', ( #19541, #21285, #22026, #1886, #24092, #10176, #2641 ) ) ;
#21654=ADVANCED_FACE ( 'NONE', ( #19686 ), #6281, .F. ) ;
#21665=CARTESIAN_POINT ( 'NONE',  ( 2.310583317527613811, 2.687712728237018567, -2.461238514389269660 ) ) ;
#21669=LINE ( 'NONE', #21545, #11669 ) ;
#21680=ORIENTED_EDGE ( 'NONE', *, *, #89, .T. ) ;
#21683=DIRECTION ( 'NONE',  ( -0.000000000000000000, -1.000000000000000000, -0.000000000000000000 ) ) ;
#21688=DIRECTION ( 'NONE',  ( 0.4999999999999912292, 0.000000000000000000, -0.8660254037844437036 ) ) ;
#21700=VECTOR ( 'NONE', #16072, 39.37007874015748143 ) ;
#21713=VERTEX_POINT ( 'NONE', #21878 ) ;
#21733=PLANE ( 'NONE',  #12514 ) ;
#21757=ORIENTED_EDGE ( 'NONE', *, *, #7836, .F. ) ;
#21761=CARTESIAN_POINT ( 'NONE',  ( 2.986000000000000210, 0.05000000000000028727, -2.541000000000000369 ) ) ;
#21762=CARTESIAN_POINT ( 'NONE',  ( 0.9384745360904206413, 2.661358883302036293, -1.341513222734410871 ) ) ;
#21763=ORIENTED_EDGE ( 'NONE', *, *, #5188, .T. ) ;
#21769=CARTESIAN_POINT ( 'NONE',  ( 0.5997114317030027841, 2.291712385858714729, -1.145928253224826276 ) ) ;
#21775=CARTESIAN_POINT ( 'NONE',  ( 2.357946643670095987, 0.000000000000000000, -2.935999999999999943 ) ) ;
#21779=EDGE_CURVE ( 'NONE', #19216, #22988, #5296, .T. ) ;
#21799=CARTESIAN_POINT ( 'NONE',  ( 1.950750485851146632, 2.384774948516263482, -1.884674727345843515 ) ) ;
#21809=EDGE_CURVE ( 'NONE', #13618, #19328, #10915, .T. ) ;
#21812=VECTOR ( 'NONE', #9752, 39.37007874015748143 ) ;
#21837=ORIENTED_EDGE ( 'NONE', *, *, #10878, .T. ) ;
#21838=EDGE_CURVE ( 'NONE', #18699, #24096, #3108, .T. ) ;
#21848=DIRECTION ( 'NONE',  ( -1.000000000000000000, 0.000000000000000000, 4.440892098500625176E-16 ) ) ;
#21849=CARTESIAN_POINT ( 'NONE',  ( 0.000000000000000000, 2.291712385858714729, 0.03922008423644621905 ) ) ;
#21850=VERTEX_POINT ( 'NONE', #16640 ) ;
#21854=CARTESIAN_POINT ( 'NONE',  ( 2.556721741255282954, 0.000000000000000000, -2.088288568297006265 ) ) ;
#21857=CARTESIAN_POINT ( 'NONE',  ( 0.3950000000000000733, 2.665000000000000036, -0.6331572882965880167 ) ) ;
#21859=CARTESIAN_POINT ( 'NONE',  ( 0.05000000000000014849, 2.740000000000000213, -2.078583302491978202 ) ) ;
#21869=LINE ( 'NONE', #8587, #16723 ) ;
#21874=EDGE_CURVE ( 'NONE', #24032, #5136, #11391, .T. ) ;
#21876=EDGE_LOOP ( 'NONE', ( #22858, #22006, #16546, #21154, #10309, #14421, #4082, #6364, #15284, #23594, #9954, #10040, #17835, #24009, #1549, #7734, #2679, #5531, #912, #8605, #20945, #5306, #19290, #4236 ) ) ;
#21878=CARTESIAN_POINT ( 'NONE',  ( 0.000000000000000000, 2.665000000000000036, -2.194053356329904947 ) ) ;
#21879=LINE ( 'NONE', #16039, #24056 ) ;
#21880=VERTEX_POINT ( 'NONE', #13237 ) ;
#21906=CARTESIAN_POINT ( 'NONE',  ( 0.3950000000000000178, 2.665000000000000036, -1.966000000000000192 ) ) ;
#21932=DIRECTION ( 'NONE',  ( 0.000000000000000000, 0.000000000000000000, -1.000000000000000000 ) ) ;
#21942=VECTOR ( 'NONE', #23099, 39.37007874015748143 ) ;
#21943=VERTEX_POINT ( 'NONE', #3948 ) ;
#21968=ADVANCED_FACE ( 'NONE', ( #856 ), #13349, .F. ) ;
#21969=EDGE_CURVE ( 'NONE', #5797, #22655, #9680, .T. ) ;
#21972=DIRECTION ( 'NONE',  ( -4.347502568299324428E-16, 0.7071067811865500152, -0.7071067811865451302 ) ) ;
#21976=CARTESIAN_POINT ( 'NONE',  ( 2.936000000000000387, 0.02499999999999983832, -2.566000000000001169 ) ) ;
#21978=CARTESIAN_POINT ( 'NONE',  ( 0.9473029863927551197, 2.405292355953585925, -1.303818980007233064 ) ) ;
#22005=ORIENTED_EDGE ( 'NONE', *, *, #97, .T. ) ;
#22006=ORIENTED_EDGE ( 'NONE', *, *, #3179, .T. ) ;
#22013=DIRECTION ( 'NONE',  ( -0.6121567523560114132, -0.6746457328860028246, 0.4124527192826460964 ) ) ;
#22026=ORIENTED_EDGE ( 'NONE', *, *, #566, .T. ) ;
#22029=PLANE ( 'NONE',  #21542 ) ;
#22032=EDGE_CURVE ( 'NONE', #21850, #7051, #2922, .T. ) ;
#22035=EDGE_CURVE ( 'NONE', #6320, #12233, #12335, .T. ) ;
#22075=LINE ( 'NONE', #3663, #20002 ) ;
#22085=SHAPE_DEFINITION_REPRESENTATION ( #3297, #18521 ) ;
#22094=CARTESIAN_POINT ( 'NONE',  ( 2.986000000000000210, 2.740000000000000213, 0.000000000000000000 ) ) ;
#22101=AXIS2_PLACEMENT_3D ( 'NONE', #16206, #14372, #13901 ) ;
#22123=LINE ( 'NONE', #23946, #12832 ) ;
#22126=APPLICATION_CONTEXT ( 'configuration controlled 3d designs of mechanical parts and assemblies' ) ;
#22140=CARTESIAN_POINT ( 'NONE',  ( 0.5097595264191668862, 2.291712385858714285, -0.6667552972947643486 ) ) ;
#22141=EDGE_LOOP ( 'NONE', ( #671, #20952, #23580, #10316, #18580 ) ) ;
#22144=ORIENTED_EDGE ( 'NONE', *, *, #3042, .F. ) ;
#22145=EDGE_CURVE ( 'NONE', #9048, #22560, #14878, .T. ) ;
#22151=ORIENTED_EDGE ( 'NONE', *, *, #1550, .F. ) ;
#22168=VECTOR ( 'NONE', #2868, 39.37007874015748854 ) ;
#22171=PLANE ( 'NONE',  #10708 ) ;
#22196=ORIENTED_EDGE ( 'NONE', *, *, #3824, .T. ) ;
#22216=VECTOR ( 'NONE', #10183, 39.37007874015748143 ) ;
#22217=CARTESIAN_POINT ( 'NONE',  ( 0.4450000000000002842, 2.665000000000000036, -2.591000000000000192 ) ) ;
#22219=VECTOR ( 'NONE', #4609, 39.37007874015748143 ) ;
#22229=EDGE_CURVE ( 'NONE', #13735, #8250, #22416, .T. ) ;
#22234=ORIENTED_EDGE ( 'NONE', *, *, #13200, .T. ) ;
#22237=DIRECTION ( 'NONE',  ( 2.775557561562891967E-17, 0.7071067811865475727, 0.7071067811865474617 ) ) ;
#22261=FACE_OUTER_BOUND ( 'NONE', #19029, .T. ) ;
#22268=ORIENTED_EDGE ( 'NONE', *, *, #3360, .T. ) ;
#22270=EDGE_CURVE ( 'NONE', #12390, #13943, #12293, .T. ) ;
#22310=CIRCLE ( 'NONE', #14528, 0.4062499999999995004 ) ;
#22314=ORIENTED_EDGE ( 'NONE', *, *, #20792, .F. ) ;
#22320=DIRECTION ( 'NONE',  ( -0.6681584153635194978, 0.6681584153635199419, 0.3273051541876792481 ) ) ;
#22323=AXIS2_PLACEMENT_3D ( 'NONE', #13876, #7445, #13076 ) ;
#22325=DIRECTION ( 'NONE',  ( 0.8660254037844434816, 0.000000000000000000, 0.4999999999999913403 ) ) ;
#22351=ORIENTED_EDGE ( 'NONE', *, *, #7888, .T. ) ;
#22354=CARTESIAN_POINT ( 'NONE',  ( 2.986000000000000210, 2.664999999999999591, -2.541000000000000369 ) ) ;
#22355=VERTEX_POINT ( 'NONE', #16932 ) ;
#22382=EDGE_CURVE ( 'NONE', #20541, #22410, #23169, .T. ) ;
#22384=VERTEX_POINT ( 'NONE', #4123 ) ;
#22397=VECTOR ( 'NONE', #22237, 39.37007874015748143 ) ;
#22401=DIRECTION ( 'NONE',  ( 0.000000000000000000, 1.000000000000000000, 0.000000000000000000 ) ) ;
#22402=CARTESIAN_POINT ( 'NONE',  ( 1.652041376866375977, 2.315961009048385755, -2.060610414248980504 ) ) ;
#22410=VERTEX_POINT ( 'NONE', #15348 ) ;
#22411=FACE_OUTER_BOUND ( 'NONE', #22758, .T. ) ;
#22412=ADVANCED_FACE ( 'NONE', ( #8018 ), #229, .F. ) ;
#22416=LINE ( 'NONE', #9380, #13079 ) ;
#22434=ORIENTED_EDGE ( 'NONE', *, *, #13653, .T. ) ;
#22438=ORIENTED_EDGE ( 'NONE', *, *, #22834, .F. ) ;
#22443=FACE_OUTER_BOUND ( 'NONE', #19821, .T. ) ;
#22450=DIRECTION ( 'NONE',  ( -0.8660254037844434816, 0.000000000000000000, 0.4999999999999916178 ) ) ;
#22469=VECTOR ( 'NONE', #8292, 39.37007874015748854 ) ;
#22470=ORIENTED_EDGE ( 'NONE', *, *, #5893, .T. ) ;
#22473=DIRECTION ( 'NONE',  ( 0.5000000000000037748, 0.000000000000000000, 0.8660254037844362651 ) ) ;
#22474=( NAMED_UNIT ( * ) PLANE_ANGLE_UNIT ( ) SI_UNIT ( $, .RADIAN. ) );
#22477=EDGE_CURVE ( 'NONE', #13943, #12390, #18126, .T. ) ;
#22491=CARTESIAN_POINT ( 'NONE',  ( 0.3635541710483937705, 0.08144582895160552838, -0.3889703289146366760 ) ) ;
#22494=DIRECTION ( 'NONE',  ( -0.5000000000000037748, 0.000000000000000000, -0.8660254037844362651 ) ) ;
#22529=LINE ( 'NONE', #18754, #5773 ) ;
#22530=FACE_OUTER_BOUND ( 'NONE', #12268, .T. ) ;
#22533=ORIENTED_EDGE ( 'NONE', *, *, #7391, .F. ) ;
#22549=CARTESIAN_POINT ( 'NONE',  ( 2.306251239869411052, 2.690142902515283208, -2.514111228547471377 ) ) ;
#22560=VERTEX_POINT ( 'NONE', #10586 ) ;
#22587=EDGE_CURVE ( 'NONE', #2181, #15406, #15789, .T. ) ;
#22610=ORIENTED_EDGE ( 'NONE', *, *, #7888, .F. ) ;
#22615=CYLINDRICAL_SURFACE ( 'NONE', #341, 0.4062499999999997780 ) ;
#22618=ORIENTED_EDGE ( 'NONE', *, *, #6146, .F. ) ;
#22649=FACE_OUTER_BOUND ( 'NONE', #13721, .T. ) ;
#22655=VERTEX_POINT ( 'NONE', #8862 ) ;
#22662=ORIENTED_EDGE ( 'NONE', *, *, #22270, .T. ) ;
#22667=CARTESIAN_POINT ( 'NONE',  ( 2.952666666666668327, 2.723333333333333606, -0.03333333333333364512 ) ) ;
#22697=EDGE_CURVE ( 'NONE', #23979, #16523, #9231, .T. ) ;
#22698=LINE ( 'NONE', #18801, #5978 ) ;
#22706=FACE_OUTER_BOUND ( 'NONE', #10129, .T. ) ;
#22713=EDGE_CURVE ( 'NONE', #21880, #20052, #1908, .T. ) ;
#22731=DIRECTION ( 'NONE',  ( 0.4999999999999919509, 0.000000000000000000, 0.8660254037844431485 ) ) ;
#22740=ORIENTED_EDGE ( 'NONE', *, *, #5216, .T. ) ;
#22743=ORIENTED_EDGE ( 'NONE', *, *, #13083, .F. ) ;
#22746=ORIENTED_EDGE ( 'NONE', *, *, #9881, .T. ) ;
#22750=CARTESIAN_POINT ( 'NONE',  ( 1.573500000000000343, 2.740000000000000213, -1.412500000000000089 ) ) ;
#22758=EDGE_LOOP ( 'NONE', ( #7014, #21611, #11545, #18198 ) ) ;
#22770=CARTESIAN_POINT ( 'NONE',  ( 2.100416254512341485, 2.978485840173427324, -2.201288568297000925 ) ) ;
#22801=CARTESIAN_POINT ( 'NONE',  ( 1.124754269082862912, 2.291712385858714285, -0.4073223533918538530 ) ) ;
#22819=FACE_OUTER_BOUND ( 'NONE', #17020, .T. ) ;
#22827=EDGE_CURVE ( 'NONE', #1154, #12827, #20686, .T. ) ;
#22828=LINE ( 'NONE', #11626, #10638 ) ;
#22829=ORIENTED_EDGE ( 'NONE', *, *, #1557, .T. ) ;
#22830=CARTESIAN_POINT ( 'NONE',  ( 0.7847114317029993957, 2.291712385858714285, -0.8254988538245819907 ) ) ;
#22834=EDGE_CURVE ( 'NONE', #397, #21142, #9594, .T. ) ;
#22850=LINE ( 'NONE', #17133, #20884 ) ;
#22858=ORIENTED_EDGE ( 'NONE', *, *, #22032, .F. ) ;
#22860=ORIENTED_EDGE ( 'NONE', *, *, #7333, .F. ) ;
#22864=ORIENTED_EDGE ( 'NONE', *, *, #9482, .F. ) ;
#22880=DIRECTION ( 'NONE',  ( 0.8660254037844360431, 0.000000000000000000, 0.5000000000000043299 ) ) ;
#22884=AXIS2_PLACEMENT_3D ( 'NONE', #19704, #12410, #695 ) ;
#22897=ORIENTED_EDGE ( 'NONE', *, *, #8017, .T. ) ;
#22924=PLANE ( 'NONE',  #13055 ) ;
#22928=DIRECTION ( 'NONE',  ( 0.5000000000000007772, 0.000000000000000000, 0.8660254037844382635 ) ) ;
#22958=CARTESIAN_POINT ( 'NONE',  ( 0.4450000000000002842, 0.000000000000000000, -2.540999999999999925 ) ) ;
#22960=ORIENTED_EDGE ( 'NONE', *, *, #9157, .T. ) ;
#22962=AXIS2_PLACEMENT_3D ( 'NONE', #11179, #13143, #14845 ) ;
#22977=PLANE ( 'NONE',  #20054 ) ;
#22978=FACE_OUTER_BOUND ( 'NONE', #21642, .T. ) ;
#22981=EDGE_CURVE ( 'NONE', #22355, #2961, #14581, .T. ) ;
#22988=VERTEX_POINT ( 'NONE', #11164 ) ;
#22996=DIRECTION ( 'NONE',  ( -0.5000000000000007772, 1.043468761970410837E-18, -0.8660254037844380415 ) ) ;
#23001=ORIENTED_EDGE ( 'NONE', *, *, #17834, .F. ) ;
#23003=ORIENTED_EDGE ( 'NONE', *, *, #8703, .F. ) ;
#23030=LINE ( 'NONE', #8391, #21003 ) ;
#23036=DIRECTION ( 'NONE',  ( -0.8635502596144278842, -0.07555085810113110201, -0.4985709748471494618 ) ) ;
#23057=VERTEX_POINT ( 'NONE', #3471 ) ;
#23058=CARTESIAN_POINT ( 'NONE',  ( 1.573500000000000343, 0.02500000000000021302, -0.5399999999999998135 ) ) ;
#23060=DIRECTION ( 'NONE',  ( 0.8660254037844523634, -0.000000000000000000, -0.4999999999999761857 ) ) ;
#23064=ORIENTED_EDGE ( 'NONE', *, *, #19301, .F. ) ;
#23065=AXIS2_PLACEMENT_3D ( 'NONE', #17106, #11748, #4291 ) ;
#23066=DIRECTION ( 'NONE',  ( -0.8660254037844434816, -0.000000000000000000, 0.4999999999999915068 ) ) ;
#23074=PLANE ( 'NONE',  #9286 ) ;
#23075=ADVANCED_FACE ( 'NONE', ( #1762 ), #7140, .T. ) ;
#23077=CARTESIAN_POINT ( 'NONE',  ( 1.652571746775178596, 2.291712385858714285, -2.061529041877832480 ) ) ;
#23081=CARTESIAN_POINT ( 'NONE',  ( 0.000000000000000000, 2.690000000000002167, -2.986000000000000210 ) ) ;
#23083=VECTOR ( 'NONE', #7975, 39.37007874015748143 ) ;
#23089=ORIENTED_EDGE ( 'NONE', *, *, #16032, .T. ) ;
#23099=DIRECTION ( 'NONE',  ( 9.614813431917706176E-16, 0.7071067811865439090, -0.7071067811865511255 ) ) ;
#23114=ORIENTED_EDGE ( 'NONE', *, *, #11008, .T. ) ;
#23128=ORIENTED_EDGE ( 'NONE', *, *, #18843, .T. ) ;
#23136=LINE ( 'NONE', #12438, #5372 ) ;
#23141=ORIENTED_EDGE ( 'NONE', *, *, #6361, .F. ) ;
#23145=CARTESIAN_POINT ( 'NONE',  ( 0.4172595264191667486, 2.291712385858714285, -0.8269699969948853813 ) ) ;
#23161=FACE_OUTER_BOUND ( 'NONE', #13665, .T. ) ;
#23169=CIRCLE ( 'NONE', #3318, 0.2124999999999999944 ) ;
#23175=EDGE_CURVE ( 'NONE', #10339, #19216, #13801, .T. ) ;
#23181=DIRECTION ( 'NONE',  ( 0.000000000000000000, 0.000000000000000000, 1.000000000000000000 ) ) ;
#23193=PLANE ( 'NONE',  #21434 ) ;
#23197=DIRECTION ( 'NONE',  ( 0.4999999999999923395, -0.000000000000000000, 0.8660254037844431485 ) ) ;
#23198=LINE ( 'NONE', #15894, #22216 ) ;
#23207=ADVANCED_FACE ( 'NONE', ( #17451 ), #8413, .T. ) ;
#23226=CARTESIAN_POINT ( 'NONE',  ( 2.126433378146018960, 2.690142902515285428, -2.942657555934166780 ) ) ;
#23234=ORIENTED_EDGE ( 'NONE', *, *, #3105, .T. ) ;
#23250=CARTESIAN_POINT ( 'NONE',  ( 2.986000000000000210, 0.05000000000000024564, -2.541000000000000369 ) ) ;
#23276=DIRECTION ( 'NONE',  ( 0.000000000000000000, -0.7071067811865474617, 0.7071067811865476838 ) ) ;
#23278=VERTEX_POINT ( 'NONE', #6833 ) ;
#23294=DIRECTION ( 'NONE',  ( 1.000000000000000000, 0.000000000000000000, 0.000000000000000000 ) ) ;
#23303=ORIENTED_EDGE ( 'NONE', *, *, #23714, .T. ) ;
#23306=EDGE_CURVE ( 'NONE', #23447, #7051, #12042, .T. ) ;
#23320=FACE_OUTER_BOUND ( 'NONE', #3802, .T. ) ;
#23329=CARTESIAN_POINT ( 'NONE',  ( 0.9244709581221671746, 2.291712385858714729, -1.333428253224822280 ) ) ;
#23334=FACE_OUTER_BOUND ( 'NONE', #2629, .T. ) ;
#23352=CARTESIAN_POINT ( 'NONE',  ( 2.108637995767629114, 2.978485840173427324, -1.763529041877836434 ) ) ;
#23357=LINE ( 'NONE', #6428, #9614 ) ;
#23359=DIRECTION ( 'NONE',  ( 0.000000000000000000, 1.000000000000000000, 0.000000000000000000 ) ) ;
#23370=ORIENTED_EDGE ( 'NONE', *, *, #14595, .T. ) ;
#23382=LINE ( 'NONE', #17916, #9733 ) ;
#23384=DIRECTION ( 'NONE',  ( 0.000000000000000000, 0.000000000000000000, -1.000000000000000000 ) ) ;
#23386=AXIS2_PLACEMENT_3D ( 'NONE', #2322, #3697, #9063 ) ;
#23390=DIRECTION ( 'NONE',  ( -0.5773502691896257311, 0.5773502691896257311, 0.5773502691896257311 ) ) ;
#23393=DIRECTION ( 'NONE',  ( 0.8660254037844434816, 2.725147086360870403E-18, -0.4999999999999913403 ) ) ;
#23406=LINE ( 'NONE', #21589, #21034 ) ;
#23418=EDGE_CURVE ( 'NONE', #23057, #1943, #14096, .T. ) ;
#23434=LINE ( 'NONE', #12255, #10041 ) ;
#23440=DIRECTION ( 'NONE',  ( -0.000000000000000000, -0.9961946980917454342, 0.08715574274765830465 ) ) ;
#23443=EDGE_CURVE ( 'NONE', #20947, #16517, #2753, .T. ) ;
#23447=VERTEX_POINT ( 'NONE', #21769 ) ;
#23448=VECTOR ( 'NONE', #1797, 39.37007874015747433 ) ;
#23449=VERTEX_POINT ( 'NONE', #5056 ) ;
#23469=FACE_OUTER_BOUND ( 'NONE', #5386, .T. ) ;
#23487=ORIENTED_EDGE ( 'NONE', *, *, #17528, .F. ) ;
#23490=FACE_BOUND ( 'NONE', #9816, .T. ) ;
#23494=AXIS2_PLACEMENT_3D ( 'NONE', #2466, #4526, #19401 ) ;
#23509=CARTESIAN_POINT ( 'NONE',  ( 0.5997114317030027841, 0.000000000000000000, -0.9454293994002404000 ) ) ;
#23515=PLANE ( 'NONE',  #19355 ) ;
#23533=VECTOR ( 'NONE', #17384, 39.37007874015748143 ) ;
#23541=ORIENTED_EDGE ( 'NONE', *, *, #2741, .F. ) ;
#23547=DIRECTION ( 'NONE',  ( 0.08715574274765830465, -0.9961946980917454342, -3.870492493070289564E-17 ) ) ;
#23548=PLANE ( 'NONE',  #16386 ) ;
#23549=VECTOR ( 'NONE', #15170, 39.37007874015748143 ) ;
#23569=AXIS2_PLACEMENT_3D ( 'NONE', #17813, #23276, #6590 ) ;
#23570=EDGE_LOOP ( 'NONE', ( #14407, #9322, #14021, #23880 ) ) ;
#23580=ORIENTED_EDGE ( 'NONE', *, *, #3136, .F. ) ;
#23584=EDGE_CURVE ( 'NONE', #4696, #20991, #14714, .T. ) ;
#23594=ORIENTED_EDGE ( 'NONE', *, *, #830, .T. ) ;
#23604=EDGE_CURVE ( 'NONE', #17146, #16517, #3594, .T. ) ;
#23620=EDGE_CURVE ( 'NONE', #1154, #10162, #5786, .T. ) ;
#23653=LINE ( 'NONE', #12123, #760 ) ;
#23693=DIRECTION ( 'NONE',  ( -0.6123724356957930270, -0.7071067811865475727, 0.3535533905932765064 ) ) ;
#23704=ORIENTED_EDGE ( 'NONE', *, *, #12041, .T. ) ;
#23714=EDGE_CURVE ( 'NONE', #8250, #12518, #22850, .T. ) ;
#23742=ADVANCED_FACE ( 'NONE', ( #6019 ), #298, .F. ) ;
#23745=VECTOR ( 'NONE', #6962, 39.37007874015748854 ) ;
#23755=DIRECTION ( 'NONE',  ( -0.08715574274765833240, 0.9961946980917454342, 3.870492493070290181E-17 ) ) ;
#23770=CIRCLE ( 'NONE', #10577, 0.1850000000000000533 ) ;
#23785=VECTOR ( 'NONE', #20418, 39.37007874015748143 ) ;
#23786=ORIENTED_EDGE ( 'NONE', *, *, #16243, .F. ) ;
#23788=FACE_OUTER_BOUND ( 'NONE', #4087, .T. ) ;
#23794=CARTESIAN_POINT ( 'NONE',  ( 0.9657290084419611897, 2.439517176785165997, -1.274898457470592605 ) ) ;
#23808=ORIENTED_EDGE ( 'NONE', *, *, #18104, .F. ) ;
#23813=DIRECTION ( 'NONE',  ( 1.000000000000000000, 0.000000000000000000, 0.000000000000000000 ) ) ;
#23820=VERTEX_POINT ( 'NONE', #9818 ) ;
#23823=ORIENTED_EDGE ( 'NONE', *, *, #9458, .F. ) ;
#23832=VECTOR ( 'NONE', #9974, 39.37007874015748143 ) ;
#23841=VECTOR ( 'NONE', #12591, 39.37007874015748143 ) ;
#23850=PLANE ( 'NONE',  #2881 ) ;
#23852=LINE ( 'NONE', #20457, #4686 ) ;
#23876=CARTESIAN_POINT ( 'NONE',  ( 0.4449999999999991740, 2.740000000000000213, 0.000000000000000000 ) ) ;
#23880=ORIENTED_EDGE ( 'NONE', *, *, #9432, .F. ) ;
#23884=EDGE_CURVE ( 'NONE', #13239, #2823, #15069, .T. ) ;
#23889=DIRECTION ( 'NONE',  ( -0.4985709748471496283, -0.07555085810113111588, -0.8635502596144277732 ) ) ;
#23891=EDGE_LOOP ( 'NONE', ( #20640, #1793, #23141, #6960 ) ) ;
#23896=VECTOR ( 'NONE', #1440, 39.37007874015748143 ) ;
#23897=CARTESIAN_POINT ( 'NONE',  ( 0.7463359724041155330, 0.2080000000000005456, -2.749000000000000554 ) ) ;
#23912=LINE ( 'NONE', #18081, #12241 ) ;
#23946=CARTESIAN_POINT ( 'NONE',  ( 0.8977114317029943891, 0.000000000000000000, -0.4292782587447178111 ) ) ;
#23961=VECTOR ( 'NONE', #7022, 39.37007874015748143 ) ;
#23979=VERTEX_POINT ( 'NONE', #5502 ) ;
#23982=CARTESIAN_POINT ( 'NONE',  ( 1.020000000000000018, 0.05000000000000028727, -2.591000000000000192 ) ) ;
#24009=ORIENTED_EDGE ( 'NONE', *, *, #4739, .T. ) ;
#24028=CARTESIAN_POINT ( 'NONE',  ( 0.000000000000000000, 0.05000000000000028727, 0.000000000000000000 ) ) ;
#24032=VERTEX_POINT ( 'NONE', #15021 ) ;
#24035=LINE ( 'NONE', #10775, #11321 ) ;
#24041=CARTESIAN_POINT ( 'NONE',  ( 1.108892417209500936, 2.340112590966282546, -1.018235385338814192 ) ) ;
#24049=PLANE ( 'NONE',  #23386 ) ;
#24056=VECTOR ( 'NONE', #19567, 39.37007874015748143 ) ;
#24062=VERTEX_POINT ( 'NONE', #15166 ) ;
#24065=CARTESIAN_POINT ( 'NONE',  ( 2.986000000000000210, 2.690000000000002167, -0.07500000000000014988 ) ) ;
#24091=VECTOR ( 'NONE', #18753, 39.37007874015748143 ) ;
#24092=ORIENTED_EDGE ( 'NONE', *, *, #2915, .F. ) ;
#24096=VERTEX_POINT ( 'NONE', #401 ) ;
#24104=CARTESIAN_POINT ( 'NONE',  ( 1.573500000000000343, 2.683750000000000746, -1.412500000000000089 ) ) ;
#24105=CARTESIAN_POINT ( 'NONE',  ( 1.908027509798675192, 2.439495096761425508, -1.906576846642106027 ) ) ;
#24111=VECTOR ( 'NONE', #10131, 39.37007874015748854 ) ;
#24117=ADVANCED_FACE ( 'NONE', ( #6123 ), #279, .F. ) ;
#24173=COLOUR_RGB('Black', 0.09019608, 0.27058824, 0.51372549);
#24174=FILL_AREA_STYLE_COLOUR('',#24173);
#24175=FILL_AREA_STYLE('',(#24174));
#24176=SURFACE_STYLE_FILL_AREA(#24175);
#24177=SURFACE_SIDE_STYLE('',(#24176));
#24178=SURFACE_STYLE_USAGE(.BOTH.,#24177);
#24179=PRESENTATION_STYLE_ASSIGNMENT((#24178));
#24182=STYLED_ITEM('',(#24179),#9145);
#24183=MECHANICAL_DESIGN_GEOMETRIC_PRESENTATION_REPRESENTATION('',(#24182),#558);
ENDSEC;
END-ISO-10303-21;
